ISO-10303-21;
HEADER;
FILE_DESCRIPTION (('STEP AP214'),
    '1' );
FILE_NAME ('hex flange bolt small_iso_ISO 4162 - M5 x 40 x 16-N.step',
    '2026-10-31T03:44:21',
    ( '' ),
    ( '' ),
    'SwSTEP 2.0',
    'SolidWorks 2026',
    '' );
FILE_SCHEMA (( 'AUTOMOTIVE_DESIGN' ));
ENDSEC;

DATA;
#4=CARTESIAN_POINT ( 'NONE',  ( 3.972066048304701891, -2.740530939476090388, 2.384802634787825504 ) ) ;
#8=DIRECTION ( 'NONE',  ( 0.000000000000000000, 0.000000000000000000, 1.000000000000000000 ) ) ;
#19=CARTESIAN_POINT ( 'NONE',  ( 0.000000000000000000, -3.031088913245534755, -1.750000000000001332 ) ) ;
#110=CARTESIAN_POINT ( 'NONE',  ( 3.961551342853669944, 3.742715940867779700, -0.5174258321190529086 ) ) ;
#131=ORIENTED_EDGE ( 'NONE', *, *, #8892, .F. ) ;
#150=ORIENTED_EDGE ( 'NONE', *, *, #5080, .F. ) ;
#160=PRODUCT_DEFINITION ( 'UNKNOWN', '', #4804, #10473 ) ;
#184=EDGE_CURVE ( 'NONE', #2510, #7366, #17139, .T. ) ;
#186=EDGE_CURVE ( 'NONE', #9539, #16928, #1996, .T. ) ;
#207=CARTESIAN_POINT ( 'NONE',  ( 5.599999999999999645, 0.000000000000000000, 0.000000000000000000 ) ) ;
#213=DIRECTION ( 'NONE',  ( -1.000000000000000000, -0.000000000000000000, 0.000000000000000000 ) ) ;
#255=CONICAL_SURFACE ( 'NONE', #13715, 2.055000000000000160, 0.7853981633974400633 ) ;
#275=( NAMED_UNIT ( * ) PLANE_ANGLE_UNIT ( ) SI_UNIT ( $, .RADIAN. ) );
#286=AXIS2_PLACEMENT_3D ( 'NONE', #15850, #18712, #8496 ) ;
#292=ADVANCED_FACE ( 'NONE', ( #12553 ), #11732, .T. ) ;
#293=CARTESIAN_POINT ( 'NONE',  ( 0.000000000000000000, 3.061616997868383634E-16, -2.500000000000000444 ) ) ;
#294=EDGE_CURVE ( 'NONE', #606, #16278, #14874, .T. ) ;
#306=EDGE_CURVE ( 'NONE', #15034, #6054, #602, .T. ) ;
#312=DIRECTION ( 'NONE',  ( 1.000000000000000000, 0.000000000000000000, 0.000000000000000000 ) ) ;
#331=CIRCLE ( 'NONE', #9396, 2.500000000000000444 ) ;
#344=EDGE_CURVE ( 'NONE', #16928, #11423, #12506, .T. ) ;
#349=CONICAL_SURFACE ( 'NONE', #11281, 5.371010071662833063, 1.221730476396037490 ) ;
#372=( NAMED_UNIT ( * ) SI_UNIT ( $, .STERADIAN. ) SOLID_ANGLE_UNIT ( ) );
#386=ORIENTED_EDGE ( 'NONE', *, *, #1313, .F. ) ;
#405=CARTESIAN_POINT ( 'NONE',  ( 4.050823680195224874, 3.779313952391379239, -0.5899027668435166127 ) ) ;
#414=CARTESIAN_POINT ( 'NONE',  ( 4.071447262713887127, 2.020725942163688504, 3.500000000000000000 ) ) ;
#443=CARTESIAN_POINT ( 'NONE',  ( 4.175813232069150338, -4.122719923832746325, 2.362127131240695889E-16 ) ) ;
#452=AXIS2_PLACEMENT_3D ( 'NONE', #12070, #1596, #13548 ) ;
#455=CARTESIAN_POINT ( 'NONE',  ( 4.071447262713887127, 2.020725942163686284, -3.499999999999999556 ) ) ;
#468=VERTEX_POINT ( 'NONE', #1547 ) ;
#470=VECTOR ( 'NONE', #5124, 1000.000000000000000 ) ;
#489=DIRECTION ( 'NONE',  ( 1.000000000000000000, 0.000000000000000000, 0.000000000000000000 ) ) ;
#497=CARTESIAN_POINT ( 'NONE',  ( 45.60000000000000142, 0.000000000000000000, 0.000000000000000000 ) ) ;
#502=CARTESIAN_POINT ( 'NONE',  ( 3.806834918298644066, 1.084202172485504434E-15, 3.500000000000000000 ) ) ;
#546=CARTESIAN_POINT ( 'NONE',  ( 4.180232103119976728, 2.085387772176679366, -3.570466442734698820 ) ) ;
#549=CARTESIAN_POINT ( 'NONE',  ( 4.175572532730929431, 2.061029303918044064, -3.569807470274393602 ) ) ;
#565=CARTESIAN_POINT ( 'NONE',  ( 7.547063560035813063E-16, -3.202582148906732762, -1.452965002680431272 ) ) ;
#593=DIRECTION ( 'NONE',  ( -1.000000000000000000, -0.000000000000000000, -0.000000000000000000 ) ) ;
#602=B_SPLINE_CURVE_WITH_KNOTS ( 'NONE', 3,
 ( #12165, #19041, #11456, #9987, #5485, #17465 ),
 .UNSPECIFIED., .F., .F.,
 ( 4, 2, 4 ),
 ( 0.01103795672827925789, 0.01206113196748797960, 0.01308430720669670130 ),
 .UNSPECIFIED. ) ;
#606=VERTEX_POINT ( 'NONE', #12312 ) ;
#631=CARTESIAN_POINT ( 'NONE',  ( 3.948095570617042860, 0.6965071952218068185, 3.500000000000155875 ) ) ;
#646=CARTESIAN_POINT ( 'NONE',  ( 4.132952817037867987, 2.031684012687259511, -3.518979934899751694 ) ) ;
#652=ADVANCED_FACE ( 'NONE', ( #12498 ), #3409, .F. ) ;
#669=EDGE_CURVE ( 'NONE', #11235, #2243, #10628, .T. ) ;
#675=CARTESIAN_POINT ( 'NONE',  ( -2.852594293689151105E-15, 3.375361811986501426, -1.153701847711632311 ) ) ;
#687=DIRECTION ( 'NONE',  ( -1.000000000000000000, -0.000000000000000000, -0.000000000000000000 ) ) ;
#713=CARTESIAN_POINT ( 'NONE',  ( 4.124214193018075569, -2.028338413290941666, 3.513185186763556622 ) ) ;
#732=ORIENTED_EDGE ( 'NONE', *, *, #14030, .F. ) ;
#748=EDGE_CURVE ( 'NONE', #6937, #6699, #5739, .T. ) ;
#750=ORIENTED_EDGE ( 'NONE', *, *, #344, .F. ) ;
#755=CARTESIAN_POINT ( 'NONE',  ( 4.050880675075949178, 1.379097446046194220, 3.567934390854430760 ) ) ;
#758=CIRCLE ( 'NONE', #18298, 0.4999999999999978351 ) ;
#759=DIRECTION ( 'NONE',  ( 0.3420201433256622736, 1.150791560227853228E-16, 0.9396926207859106484 ) ) ;
#762=VERTEX_POINT ( 'NONE', #17709 ) ;
#792=CARTESIAN_POINT ( 'NONE',  ( 4.175572532730932096, 4.122058607836116551, 1.170198429493232648E-15 ) ) ;
#807=CARTESIAN_POINT ( 'NONE',  ( 4.142654963991859063, -2.035398498734348305, 3.525413613457315076 ) ) ;
#814=DIRECTION ( 'NONE',  ( -1.000000000000000000, -0.000000000000000000, -0.000000000000000000 ) ) ;
#837=CARTESIAN_POINT ( 'NONE',  ( 4.086262841041386373, 2.102637316508698451, -3.499999999999999556 ) ) ;
#908=CARTESIAN_POINT ( 'NONE',  ( 4.180345304246197990, -2.049116244671341569, 3.591763845239312136 ) ) ;
#988=CARTESIAN_POINT ( 'NONE',  ( 4.151274195509680354, 4.079825909417489349, 1.184320329358001550E-15 ) ) ;
#1047=DIRECTION ( 'NONE',  ( 0.000000000000000000, 0.000000000000000000, -1.000000000000000000 ) ) ;
#1064=CARTESIAN_POINT ( 'NONE',  ( 0.3126073911696427010, 4.041451884327382338, -6.521455134176256610E-17 ) ) ;
#1067=B_SPLINE_CURVE_WITH_KNOTS ( 'NONE', 3,
 ( #18745, #1186, #18949, #15989, #2579, #5692, #9798, #9892, #15794, #10094, #9699, #2375, #18852, #11459, #17572, #2672 ),
 .UNSPECIFIED., .F., .F.,
 ( 4, 3, 3, 3, 3, 4 ),
 ( 0.000000000000000000, 3.315506744709148100E-05, 6.608280158698798419E-05, 0.0001026520855291344940, 0.0001376952025664800986, 0.0001398064759190609653 ),
 .UNSPECIFIED. ) ;
#1084=AXIS2_PLACEMENT_3D ( 'NONE', #18947, #19044, #14502 ) ;
#1093=CARTESIAN_POINT ( 'NONE',  ( 4.114405500665255566, -2.025575754679718177, -3.508400121684934980 ) ) ;
#1138=FACE_OUTER_BOUND ( 'NONE', #18234, .T. ) ;
#1186=CARTESIAN_POINT ( 'NONE',  ( 4.082498951862916670, 2.020725942163688504, 3.500000000000000000 ) ) ;
#1189=MECHANICAL_DESIGN_GEOMETRIC_PRESENTATION_REPRESENTATION('',(#10238),#17161);
#1192=CARTESIAN_POINT ( 'NONE',  ( 4.170895651974849017, -2.054890354522642237, -3.559174498016357102 ) ) ;
#1222=EDGE_LOOP ( 'NONE', ( #4222, #8069, #18986 ) ) ;
#1227=B_SPLINE_CURVE_WITH_KNOTS ( 'NONE', 3,
 ( #18034, #4596, #1560, #11644, #4300 ),
 .UNSPECIFIED., .F., .F.,
 ( 4, 1, 4 ),
 ( 5.337851785822274535E-20, 0.002020725942163691374, 0.004041451884327382747 ),
 .UNSPECIFIED. ) ;
#1285=DIRECTION ( 'NONE',  ( -1.000000000000000000, -0.000000000000000000, -0.000000000000000000 ) ) ;
#1297=SHAPE_REPRESENTATION ( 'hex flange bolt small_iso_ISO 4162 - M5 x 40 x 16-N', ( #10359 ), #10908 ) ;
#1313=EDGE_CURVE ( 'NONE', #2243, #15034, #11481, .T. ) ;
#1347=CARTESIAN_POINT ( 'NONE',  ( 4.175813232069146785, 2.061359961916365613, -3.570380186727397653 ) ) ;
#1366=ORIENTED_EDGE ( 'NONE', *, *, #7879, .F. ) ;
#1372=CARTESIAN_POINT ( 'NONE',  ( 0.3126073911696407026, -2.020725942163686728, 3.500000000000000444 ) ) ;
#1384=CARTESIAN_POINT ( 'NONE',  ( 4.086376042167605860, 1.979461949354204719, -3.571471332069177773 ) ) ;
#1422=AXIS2_PLACEMENT_3D ( 'NONE', #16165, #17937, #8987 ) ;
#1527=DIRECTION ( 'NONE',  ( 1.000000000000000000, 0.000000000000000000, -0.000000000000000000 ) ) ;
#1547=CARTESIAN_POINT ( 'NONE',  ( 4.071447262713890680, -4.041451884327386779, 0.000000000000000000 ) ) ;
#1555=VERTEX_POINT ( 'NONE', #13348 ) ;
#1560=CARTESIAN_POINT ( 'NONE',  ( 3.806834918298644954, 3.031088913245535199, -1.749999999999998446 ) ) ;
#1561=( NAMED_UNIT ( * ) SI_UNIT ( $, .STERADIAN. ) SOLID_ANGLE_UNIT ( ) );
#1573=CARTESIAN_POINT ( 'NONE',  ( -1.372193374551966155E-15, -2.859595677584338969, 2.047034997319577609 ) ) ;
#1582=FACE_OUTER_BOUND ( 'NONE', #11524, .T. ) ;
#1592=AXIS2_PLACEMENT_3D ( 'NONE', #15790, #2371, #14304 ) ;
#1596=DIRECTION ( 'NONE',  ( 1.000000000000000000, 0.000000000000000000, 0.000000000000000000 ) ) ;
#1637=ORIENTED_EDGE ( 'NONE', *, *, #8002, .F. ) ;
#1642=DIRECTION ( 'NONE',  ( 0.000000000000000000, 1.000000000000000000, -1.073081856240829552E-16 ) ) ;
#1667=ORIENTED_EDGE ( 'NONE', *, *, #4858, .F. ) ;
#1671=CARTESIAN_POINT ( 'NONE',  ( 4.630153689607048761, 0.000000000000000000, -5.371010071662833063 ) ) ;
#1683=CARTESIAN_POINT ( 'NONE',  ( 4.052424581287787042, 2.393186648133419414, -2.990837702970412959 ) ) ;
#1688=CARTESIAN_POINT ( 'NONE',  ( 0.000000000000000000, -3.031088913245534755, -1.750000000000001332 ) ) ;
#1692=DIRECTION ( 'NONE',  ( 1.000000000000000000, 0.000000000000000000, -0.000000000000000000 ) ) ;
#1697=CARTESIAN_POINT ( 'NONE',  ( 4.086262629614029862, -1.979770830881092181, -3.570936333571104626 ) ) ;
#1723=CARTESIAN_POINT ( 'NONE',  ( 0.3126073911695746443, -2.020725942163797750, -3.499999999999999556 ) ) ;
#1783=EDGE_CURVE ( 'NONE', #9539, #14693, #1067, .T. ) ;
#1785=CARTESIAN_POINT ( 'NONE',  ( 4.630153689607048761, 0.000000000000000000, 0.000000000000000000 ) ) ;
#1843=ORIENTED_EDGE ( 'NONE', *, *, #1783, .F. ) ;
#1847=EDGE_CURVE ( 'NONE', #17135, #14839, #3874, .T. ) ;
#1849=CARTESIAN_POINT ( 'NONE',  ( 3.973110223767137850, 2.263269463293572928E-11, 3.565797985667434222 ) ) ;
#1877=CARTESIAN_POINT ( 'NONE',  ( 0.000000000000000000, 0.000000000000000000, 0.000000000000000000 ) ) ;
#1889=CARTESIAN_POINT ( 'NONE',  ( 3.951447005078450037, -1.347150628109123893, 3.500000000000000888 ) ) ;
#1899=VECTOR ( 'NONE', #16556, 1000.000000000000000 ) ;
#1906=CARTESIAN_POINT ( 'NONE',  ( 4.158806965674310518, -4.075748668183988066, -0.05940377217583901054 ) ) ;
#1919=AXIS2_PLACEMENT_3D ( 'NONE', #8871, #10142, #14853 ) ;
#1936=CARTESIAN_POINT ( 'NONE',  ( 3.878104551856474735, -0.7018542299754126912, -3.499999999999999556 ) ) ;
#1939=CARTESIAN_POINT ( 'NONE',  ( 4.114405500665261783, 2.025575754679710627, -3.508400121684937645 ) ) ;
#1958=CARTESIAN_POINT ( 'NONE',  ( 4.630153689607048761, 0.000000000000000000, 0.000000000000000000 ) ) ;
#1969=DIRECTION ( 'NONE',  ( 0.000000000000000000, 0.000000000000000000, -1.000000000000000000 ) ) ;
#1996=B_SPLINE_CURVE_WITH_KNOTS ( 'NONE', 3,
 ( #14008, #4820, #5004, #15304, #15400 ),
 .UNSPECIFIED., .F., .F.,
 ( 4, 1, 4 ),
 ( 0.000000000000000000, 0.002020725942163690940, 0.004041451884327382747 ),
 .UNSPECIFIED. ) ;
#2017=ORIENTED_EDGE ( 'NONE', *, *, #16957, .T. ) ;
#2054=DIRECTION ( 'NONE',  ( -1.000000000000000000, -0.000000000000000000, -0.000000000000000000 ) ) ;
#2070=DIRECTION ( 'NONE',  ( -1.000000000000000000, -0.000000000000000000, -0.000000000000000000 ) ) ;
#2105=EDGE_CURVE ( 'NONE', #6699, #606, #12533, .T. ) ;
#2118=ORIENTED_EDGE ( 'NONE', *, *, #18878, .F. ) ;
#2123=CARTESIAN_POINT ( 'NONE',  ( 3.974175853610013132, 2.726149789692839054, 2.409821656223150033 ) ) ;
#2124=CARTESIAN_POINT ( 'NONE',  ( 4.082498951862920222, -4.041451884327386779, 0.000000000000000000 ) ) ;
#2206=ORIENTED_EDGE ( 'NONE', *, *, #17255, .F. ) ;
#2231=CARTESIAN_POINT ( 'NONE',  ( 4.175326769692858875, -4.121399112977860213, 3.677815466159040336E-14 ) ) ;
#2243=VERTEX_POINT ( 'NONE', #6942 ) ;
#2287=B_SPLINE_CURVE_WITH_KNOTS ( 'NONE', 3,
 ( #9702, #1889, #502, #7860, #414 ),
 .UNSPECIFIED., .F., .F.,
 ( 4, 1, 4 ),
 ( 0.000000000000000000, 0.002020725942163687470, 0.004041451884327374941 ),
 .UNSPECIFIED. ) ;
#2324=CARTESIAN_POINT ( 'NONE',  ( 3.958484000407329617, 3.734437307742037415, 0.5317648453100634054 ) ) ;
#2335=FACE_OUTER_BOUND ( 'NONE', #7002, .T. ) ;
#2345=VECTOR ( 'NONE', #15401, 1000.000000000000000 ) ;
#2353=CARTESIAN_POINT ( 'NONE',  ( 0.1217565302851100623, 3.710888496608919507, -0.5725525826504660465 ) ) ;
#2366=ORIENTED_EDGE ( 'NONE', *, *, #5865, .T. ) ;
#2371=DIRECTION ( 'NONE',  ( -1.000000000000000000, -0.000000000000000000, -0.000000000000000000 ) ) ;
#2375=CARTESIAN_POINT ( 'NONE',  ( 4.170895651974848128, 2.054890354522668439, 3.559174498016340227 ) ) ;
#2392=VECTOR ( 'NONE', #2054, 1000.000000000000000 ) ;
#2408=EDGE_LOOP ( 'NONE', ( #14780, #2520, #10341, #150 ) ) ;
#2425=DIRECTION ( 'NONE',  ( -0.7071067811865533459, 8.659560562354861368E-17, -0.7071067811865416886 ) ) ;
#2456=CIRCLE ( 'NONE', #7754, 2.500000000000000444 ) ;
#2476=CARTESIAN_POINT ( 'NONE',  ( 0.3126073911696408136, 2.020725942163688060, 3.500000000000000000 ) ) ;
#2494=ORIENTED_EDGE ( 'NONE', *, *, #186, .T. ) ;
#2495=CARTESIAN_POINT ( 'NONE',  ( 4.180231891692622881, -4.134807952925578789, -0.02076457676760693274 ) ) ;
#2496=B_SPLINE_CURVE_WITH_KNOTS ( 'NONE', 3,
 ( #10548, #11730, #12027, #16261, #2744 ),
 .UNSPECIFIED., .F., .F.,
 ( 4, 1, 4 ),
 ( 0.000000000000000000, 0.002020725942163690506, 0.004041451884327381013 ),
 .UNSPECIFIED. ) ;
#2510=VERTEX_POINT ( 'NONE', #16844 ) ;
#2514=AXIS2_PLACEMENT_3D ( 'NONE', #1877, #489, #1969 ) ;
#2520=ORIENTED_EDGE ( 'NONE', *, *, #8892, .T. ) ;
#2530=FACE_OUTER_BOUND ( 'NONE', #13443, .T. ) ;
#2579=CARTESIAN_POINT ( 'NONE',  ( 4.114405500665256454, 2.025575754679711959, 3.508400121684935424 ) ) ;
#2630=CARTESIAN_POINT ( 'NONE',  ( 4.630153689607048761, 0.000000000000000000, 0.000000000000000000 ) ) ;
#2637=ORIENTED_EDGE ( 'NONE', *, *, #9615, .T. ) ;
#2666=ORIENTED_EDGE ( 'NONE', *, *, #9256, .F. ) ;
#2672=CARTESIAN_POINT ( 'NONE',  ( 4.175813232069147674, 2.061359961916367833, 3.570380186727398097 ) ) ;
#2701=ADVANCED_FACE ( 'NONE', ( #16409 ), #3927, .F. ) ;
#2732=EDGE_LOOP ( 'NONE', ( #5047, #2637, #10170 ) ) ;
#2744=CARTESIAN_POINT ( 'NONE',  ( 4.071447262713888016, -2.020725942163694722, -3.499999999999999556 ) ) ;
#2757=ORIENTED_EDGE ( 'NONE', *, *, #14030, .T. ) ;
#2776=AXIS2_PLACEMENT_3D ( 'NONE', #14016, #5202, #15600 ) ;
#2796=ORIENTED_EDGE ( 'NONE', *, *, #6179, .F. ) ;
#2849=AXIS2_PLACEMENT_3D ( 'NONE', #7793, #16734, #10920 ) ;
#2853=ORIENTED_EDGE ( 'NONE', *, *, #5080, .T. ) ;
#2864=DIRECTION ( 'NONE',  ( -1.000000000000000000, -0.000000000000000000, -0.000000000000000000 ) ) ;
#2871=CARTESIAN_POINT ( 'NONE',  ( 0.000000000000000000, 0.000000000000000000, 0.000000000000000000 ) ) ;
#2889=CARTESIAN_POINT ( 'NONE',  ( 4.086376042167608524, -4.082715877136868343, 0.07147133206917789805 ) ) ;
#2894=CARTESIAN_POINT ( 'NONE',  ( 5.599999999999999645, -2.020725942163686284, 3.500000000000000444 ) ) ;
#2927=CARTESIAN_POINT ( 'NONE',  ( 0.000000000000000000, 0.000000000000000000, 0.000000000000000000 ) ) ;
#2930=LINE ( 'NONE', #13404, #14835 ) ;
#2950=CARTESIAN_POINT ( 'NONE',  ( 5.599999999999999645, 2.020725942163686284, -3.499999999999999556 ) ) ;
#2959=CARTESIAN_POINT ( 'NONE',  ( 4.158413352280807551, -2.044871626972826650, -3.541821552872960410 ) ) ;
#2960=CARTESIAN_POINT ( 'NONE',  ( 3.950241966887845457, 3.393956070637746514, -1.121495646998088569 ) ) ;
#2976=CARTESIAN_POINT ( 'NONE',  ( 3.948103430090710297, -3.379418997638724331, -1.146674596026246551 ) ) ;
#2985=ORIENTED_EDGE ( 'NONE', *, *, #1313, .T. ) ;
#2990=EDGE_LOOP ( 'NONE', ( #14866, #3846 ) ) ;
#2991=AXIS2_PLACEMENT_3D ( 'NONE', #18459, #213, #18562 ) ;
#3009=ORIENTED_EDGE ( 'NONE', *, *, #14539, .T. ) ;
#3045=CARTESIAN_POINT ( 'NONE',  ( 4.030867648406620596, -2.329326259789657350, 2.965488570640411492 ) ) ;
#3049=ADVANCED_FACE ( 'NONE', ( #15446 ), #8029, .F. ) ;
#3053=CARTESIAN_POINT ( 'NONE',  ( 45.60000000000000142, 0.000000000000000000, 0.000000000000000000 ) ) ;
#3059=CARTESIAN_POINT ( 'NONE',  ( 4.180231891692620216, 4.134807952925572572, 0.02076457676760539231 ) ) ;
#3060=DIRECTION ( 'NONE',  ( -1.000000000000000000, -0.000000000000000000, 0.000000000000000000 ) ) ;
#3065=CARTESIAN_POINT ( 'NONE',  ( 0.3126073911695746443, -2.020725942163797750, -3.499999999999999556 ) ) ;
#3079=CARTESIAN_POINT ( 'NONE',  ( 4.033901012035484790, -2.321269032827465661, -2.979444097106959788 ) ) ;
#3095=AXIS2_PLACEMENT_3D ( 'NONE', #17267, #15977, #11647 ) ;
#3104=CARTESIAN_POINT ( 'NONE',  ( 3.973110223767137850, -2.261493176400255405E-11, -3.565797985667433334 ) ) ;
#3120=ORIENTED_EDGE ( 'NONE', *, *, #3205, .F. ) ;
#3144=FACE_OUTER_BOUND ( 'NONE', #11069, .T. ) ;
#3154=CARTESIAN_POINT ( 'NONE',  ( 4.033901012036086087, 3.740908793663944021, -0.5205559028925770271 ) ) ;
#3186=ORIENTED_EDGE ( 'NONE', *, *, #669, .F. ) ;
#3205=EDGE_CURVE ( 'NONE', #14054, #15034, #6646, .T. ) ;
#3280=CIRCLE ( 'NONE', #14528, 3.500000000000000000 ) ;
#3297=VERTEX_POINT ( 'NONE', #14640 ) ;
#3317=B_SPLINE_CURVE_WITH_KNOTS ( 'NONE', 3,
 ( #11518, #17527, #4088, #15554 ),
 .UNSPECIFIED., .F., .F.,
 ( 4, 4 ),
 ( 2.380739282167303683E-07, 0.002044882221487525839 ),
 .UNSPECIFIED. ) ;
#3318=ORIENTED_EDGE ( 'NONE', *, *, #15393, .T. ) ;
#3329=LINE ( 'NONE', #1671, #7222 ) ;
#3370=FACE_OUTER_BOUND ( 'NONE', #18818, .T. ) ;
#3383=ORIENTED_EDGE ( 'NONE', *, *, #748, .T. ) ;
#3399=CARTESIAN_POINT ( 'NONE',  ( 4.180345304246197990, 4.135116856707394817, -0.02129519942689619277 ) ) ;
#3409=( BOUNDED_SURFACE ( )  B_SPLINE_SURFACE ( 3, 2, ( 
 ( #11218, #6715, #11321 ),
 ( #17224, #11121, #7902 ),
 ( #3685, #9752, #2123 ),
 ( #5057, #18608, #14158 ),
 ( #2324, #8277, #12801 ),
 ( #15449, #9463, #3399 ) ),
 .UNSPECIFIED., .F., .F., .F. ) 
 B_SPLINE_SURFACE_WITH_KNOTS ( ( 4, 2, 4 ),
 ( 3, 3 ),
 ( 0.01651999345535505245, 0.01858032176739834312, 0.02064065007944163727 ),
 ( 0.000000000000000000, 1.000000000000000000 ),
 .UNSPECIFIED. ) 
 GEOMETRIC_REPRESENTATION_ITEM ( )  RATIONAL_B_SPLINE_SURFACE ( (
 ( 1.000000000000000000, 0.8047781103519393575, 1.000000000000000000),
 ( 1.000000000000000000, 0.8123785825604844524, 1.000000000000000000),
 ( 1.000000000000000000, 0.8190671539787625077, 1.000000000000000000),
 ( 1.000000000000000000, 0.8192352254835536529, 1.000000000000000000),
 ( 1.000000000000000000, 0.8126129677211098024, 1.000000000000000000),
 ( 1.000000000000000000, 0.8047712537969730073, 1.000000000000000000) ) ) 
 REPRESENTATION_ITEM ( '' )  SURFACE ( )  );
#3418=DIRECTION ( 'NONE',  ( 1.000000000000000000, 0.000000000000000000, 0.000000000000000000 ) ) ;
#3498=CARTESIAN_POINT ( 'NONE',  ( 3.972073812946708582, -0.6951863858492246528, -3.565770933504603057 ) ) ;
#3500=CARTESIAN_POINT ( 'NONE',  ( 4.124214193018076458, 2.028338413290941222, -3.513185186763556622 ) ) ;
#3519=DIRECTION ( 'NONE',  ( -1.000000000000000000, -0.000000000000000000, -0.000000000000000000 ) ) ;
#3556=CARTESIAN_POINT ( 'NONE',  ( 4.165266963751724560, -2.049631966911991565, 3.550066703508907739 ) ) ;
#3584=ORIENTED_EDGE ( 'NONE', *, *, #14917, .F. ) ;
#3593=CARTESIAN_POINT ( 'NONE',  ( 4.175572532730933872, -4.122058607836120103, 1.048217341165752127E-14 ) ) ;
#3600=AXIS2_PLACEMENT_3D ( 'NONE', #18051, #1285, #7546 ) ;
#3605=CARTESIAN_POINT ( 'NONE',  ( 0.3126073911696451990, -4.041451884327386779, -1.834154111220703958E-17 ) ) ;
#3606=CIRCLE ( 'NONE', #13624, 0.4999999999999978351 ) ;
#3621=B_SPLINE_CURVE_WITH_KNOTS ( 'NONE', 3,
 ( #18128, #17014, #10905, #16913 ),
 .UNSPECIFIED., .F., .F.,
 ( 4, 4 ),
 ( 0.000000000000000000, 0.002080789711329296236 ),
 .UNSPECIFIED. ) ;
#3653=CARTESIAN_POINT ( 'NONE',  ( 4.175813232069146785, -2.061359961916366057, 3.570380186727398542 ) ) ;
#3661=DIRECTION ( 'NONE',  ( 0.000000000000000000, -1.224646799147353947E-16, 1.000000000000000000 ) ) ;
#3665=CLOSED_SHELL ( 'NONE', ( #12744, #3985, #12853, #8349, #18516, #5438, #292, #3767, #6678, #17555, #6889, #13970, #12563, #16730, #9982, #14712, #10503, #14422, #8605, #4240, #15488, #16842, #4392, #7709, #2701, #15768, #3049, #652, #7343 ) ) ;
#3670=DIRECTION ( 'NONE',  ( -0.000000000000000000, 0.000000000000000000, 1.000000000000000000 ) ) ;
#3685=CARTESIAN_POINT ( 'NONE',  ( 3.880206590543030742, 2.665671387532550618, 2.382921720510995822 ) ) ;
#3703=VERTEX_POINT ( 'NONE', #11290 ) ;
#3767=ADVANCED_FACE ( 'NONE', ( #16016 ), #18769, .F. ) ;
#3788=CARTESIAN_POINT ( 'NONE',  ( 4.124214193018072017, -4.056676826581893103, 6.968404583626299416E-17 ) ) ;
#3819=AXIS2_PLACEMENT_3D ( 'NONE', #3053, #2864, #8 ) ;
#3836=EDGE_CURVE ( 'NONE', #14054, #3297, #3280, .T. ) ;
#3839=CARTESIAN_POINT ( 'NONE',  ( 3.951447005078450925, -2.357513599190977249, -2.916666666666666519 ) ) ;
#3846=ORIENTED_EDGE ( 'NONE', *, *, #294, .T. ) ;
#3865=ORIENTED_EDGE ( 'NONE', *, *, #4848, .T. ) ;
#3874=B_SPLINE_CURVE_WITH_KNOTS ( 'NONE', 3,
 ( #6764, #6856, #12843, #3934, #14406, #2476 ),
 .UNSPECIFIED., .F., .F.,
 ( 4, 2, 4 ),
 ( 0.005852013098461904955, 0.006875955139453157790, 0.007899897180444410624 ),
 .UNSPECIFIED. ) ;
#3922=CARTESIAN_POINT ( 'NONE',  ( 0.3126073911696408136, 2.020725942163688060, 3.500000000000000000 ) ) ;
#3927=( BOUNDED_SURFACE ( )  B_SPLINE_SURFACE ( 3, 2, ( 
 ( #1697, #7380, #13553 ),
 ( #16506, #3079, #15023 ),
 ( #8849, #6106, #10701 ),
 ( #7474, #2976, #17984 ),
 ( #10308, #14824, #13454 ),
 ( #2889, #16604, #14925 ) ),
 .UNSPECIFIED., .F., .F., .T. ) 
 B_SPLINE_SURFACE_WITH_KNOTS ( ( 4, 2, 4 ),
 ( 3, 3 ),
 ( 0.01651999345535506980, 0.01858032176739836394, 0.02064065007944165808 ),
 ( 0.000000000000000000, 1.000000000000000000 ),
 .UNSPECIFIED. ) 
 GEOMETRIC_REPRESENTATION_ITEM ( )  RATIONAL_B_SPLINE_SURFACE ( (
 ( 1.000000000000000000, 0.8047781103519393575, 1.000000000000000000),
 ( 1.000000000000000000, 0.8123785825603968558, 1.000000000000000000),
 ( 1.000000000000000000, 0.8190671539788806355, 1.000000000000000000),
 ( 1.000000000000000000, 0.8192352254834333047, 1.000000000000000000),
 ( 1.000000000000000000, 0.8126129677212012847, 1.000000000000000000),
 ( 1.000000000000000000, 0.8047712537969730073, 1.000000000000000000) ) ) 
 REPRESENTATION_ITEM ( '' )  SURFACE ( )  );
#3934=CARTESIAN_POINT ( 'NONE',  ( 0.1397371499203167444, 1.362866705341264195, 3.499999999999999556 ) ) ;
#3951=CARTESIAN_POINT ( 'NONE',  ( 3.950241966888158540, -3.393956070638132871, 1.121495646998118545 ) ) ;
#3965=CARTESIAN_POINT ( 'NONE',  ( 4.055498735588912496, -1.410041617600660491, 3.568038744583366118 ) ) ;
#3984=FACE_BOUND ( 'NONE', #2990, .T. ) ;
#3985=ADVANCED_FACE ( 'NONE', ( #16500 ), #16753, .T. ) ;
#3994=EDGE_LOOP ( 'NONE', ( #17815, #2206 ) ) ;
#4066=CARTESIAN_POINT ( 'NONE',  ( 4.180345472528542494, 2.086001522971430600, 3.570468649087212398 ) ) ;
#4081=B_SPLINE_CURVE_WITH_KNOTS ( 'NONE', 3,
 ( #7936, #6008, #13825, #18168, #405, #4725 ),
 .UNSPECIFIED., .F., .F.,
 ( 4, 2, 4 ),
 ( 0.000000000000000000, 0.002086519881787260184, 0.004173039763574520368 ),
 .UNSPECIFIED. ) ;
#4088=CARTESIAN_POINT ( 'NONE',  ( -1.935715396507168721E-15, 2.686816014504566752, 2.346298152288372130 ) ) ;
#4111=CARTESIAN_POINT ( 'NONE',  ( 4.050536630291690976, 3.778525289263159781, 0.5912575323401418892 ) ) ;
#4125=EDGE_CURVE ( 'NONE', #4747, #5816, #8135, .T. ) ;
#4141=PRODUCT_DEFINITION_SHAPE ( 'NONE', 'NONE',  #160 ) ;
#4221=CARTESIAN_POINT ( 'NONE',  ( 4.175813232069148562, -2.061359961916374051, -3.570380186727397653 ) ) ;
#4222=ORIENTED_EDGE ( 'NONE', *, *, #6179, .T. ) ;
#4225=SHAPE_DEFINITION_REPRESENTATION ( #4141, #1297 ) ;
#4240=ADVANCED_FACE ( 'NONE', ( #12842 ), #18851, .F. ) ;
#4250=EDGE_LOOP ( 'NONE', ( #4254, #3383, #7149, #19103 ) ) ;
#4254=ORIENTED_EDGE ( 'NONE', *, *, #6763, .T. ) ;
#4271=CARTESIAN_POINT ( 'NONE',  ( 3.973514160553462737, -2.741076955031366502, -2.383932505289870551 ) ) ;
#4300=CARTESIAN_POINT ( 'NONE',  ( 4.071447262713887127, 2.020725942163686284, -3.499999999999999556 ) ) ;
#4309=ORIENTED_EDGE ( 'NONE', *, *, #9976, .T. ) ;
#4311=CARTESIAN_POINT ( 'NONE',  ( 0.02993401039713673023, -2.688325911136453694, 2.343682934607768775 ) ) ;
#4322=CARTESIAN_POINT ( 'NONE',  ( 4.151274195509678577, -2.039912954708747339, -3.533232880573492274 ) ) ;
#4368=EDGE_CURVE ( 'NONE', #7529, #7505, #9837, .T. ) ;
#4369=CARTESIAN_POINT ( 'NONE',  ( 4.175813232069150338, -4.122719923832746325, 2.362127131240695889E-16 ) ) ;
#4371=AXIS2_PLACEMENT_3D ( 'NONE', #16322, #5727, #8948 ) ;
#4392=ADVANCED_FACE ( 'NONE', ( #5786 ), #5990, .F. ) ;
#4415=CARTESIAN_POINT ( 'NONE',  ( 3.878096787214416530, -2.680238624820946214, 2.357690525401583415 ) ) ;
#4470=CARTESIAN_POINT ( 'NONE',  ( 4.050536630291693641, -3.778525289263164222, -0.5912575323401421112 ) ) ;
#4503=ORIENTED_EDGE ( 'NONE', *, *, #184, .T. ) ;
#4526=CARTESIAN_POINT ( 'NONE',  ( 3.878096787214415642, 2.680238624820947990, -2.357690525401575421 ) ) ;
#4596=CARTESIAN_POINT ( 'NONE',  ( 3.951447005078450925, 3.704664227300100254, -0.5833333333333329263 ) ) ;
#4606=DIRECTION ( 'NONE',  ( 0.3420201433256622736, 0.000000000000000000, -0.9396926207859106484 ) ) ;
#4634=CIRCLE ( 'NONE', #7132, 2.500000000000000444 ) ;
#4665=( GEOMETRIC_REPRESENTATION_CONTEXT ( 3 ) GLOBAL_UNCERTAINTY_ASSIGNED_CONTEXT ( ( #13615 ) ) GLOBAL_UNIT_ASSIGNED_CONTEXT ( ( #10846, #12229, #10754 ) ) REPRESENTATION_CONTEXT ( 'NONE', 'WORKASPACE' ) );
#4668=ORIENTED_EDGE ( 'NONE', *, *, #1847, .F. ) ;
#4725=CARTESIAN_POINT ( 'NONE',  ( 4.175813232069148562, 4.122719923832741884, -2.765695189283172261E-17 ) ) ;
#4726=TOROIDAL_SURFACE ( 'NONE', #15679, 5.200000000000001066, 0.4999999999999978351 ) ;
#4747=VERTEX_POINT ( 'NONE', #10072 ) ;
#4766=VERTEX_POINT ( 'NONE', #1064 ) ;
#4789=ORIENTED_EDGE ( 'NONE', *, *, #6763, .F. ) ;
#4804=PRODUCT_DEFINITION_FORMATION_WITH_SPECIFIED_SOURCE ( 'ANY', '', #11148, .NOT_KNOWN. ) ;
#4820=CARTESIAN_POINT ( 'NONE',  ( 3.951447005078450925, 2.357513599190970144, 2.916666666666667407 ) ) ;
#4848=EDGE_CURVE ( 'NONE', #9274, #6054, #13309, .T. ) ;
#4858=EDGE_CURVE ( 'NONE', #2243, #10511, #2496, .T. ) ;
#4919=FACE_OUTER_BOUND ( 'NONE', #2408, .T. ) ;
#4956=CARTESIAN_POINT ( 'NONE',  ( 4.104070371397485317, 2.023683613428364225, -3.505122836902508698 ) ) ;
#4957=CARTESIAN_POINT ( 'NONE',  ( 4.093692494532774617, -4.043567292011547742, 3.285329657490527105E-16 ) ) ;
#4973=FACE_OUTER_BOUND ( 'NONE', #2732, .T. ) ;
#4976=ORIENTED_EDGE ( 'NONE', *, *, #5015, .F. ) ;
#4997=DIRECTION ( 'NONE',  ( 0.000000000000000000, -0.8660254037844382635, -0.5000000000000008882 ) ) ;
#5004=CARTESIAN_POINT ( 'NONE',  ( 3.806834918298646731, 3.031088913245537864, 1.750000000000000666 ) ) ;
#5015=EDGE_CURVE ( 'NONE', #10511, #14216, #2930, .T. ) ;
#5034=DIRECTION ( 'NONE',  ( 0.000000000000000000, 0.000000000000000000, -1.000000000000000000 ) ) ;
#5044=LINE ( 'NONE', #2894, #18163 ) ;
#5047=ORIENTED_EDGE ( 'NONE', *, *, #17938, .T. ) ;
#5055=CARTESIAN_POINT ( 'NONE',  ( 4.033895293471413623, 1.419609371826631827, -3.500000000000000000 ) ) ;
#5057=CARTESIAN_POINT ( 'NONE',  ( 3.878096787214571517, 3.381939201670116191, 1.142309474598433461 ) ) ;
#5080=EDGE_CURVE ( 'NONE', #7529, #2510, #758, .T. ) ;
#5099=EDGE_CURVE ( 'NONE', #762, #6796, #3621, .T. ) ;
#5119=ORIENTED_EDGE ( 'NONE', *, *, #15675, .T. ) ;
#5124=DIRECTION ( 'NONE',  ( -1.000000000000000000, -0.000000000000000000, -0.000000000000000000 ) ) ;
#5202=DIRECTION ( 'NONE',  ( -1.000000000000000000, -0.000000000000000000, -0.000000000000000000 ) ) ;
#5211=CARTESIAN_POINT ( 'NONE',  ( 4.175572532730931208, -2.061029303918052946, 3.569807470274390493 ) ) ;
#5219=CARTESIAN_POINT ( 'NONE',  ( 5.599999999999999645, 2.020725942163688504, 3.500000000000000000 ) ) ;
#5232=CARTESIAN_POINT ( 'NONE',  ( 3.961557105776161158, -1.423285172354515016, 3.500000000000000444 ) ) ;
#5315=CARTESIAN_POINT ( 'NONE',  ( 4.158921614371307918, -1.986121848748762186, 3.559936047944509241 ) ) ;
#5316=CARTESIAN_POINT ( 'NONE',  ( 45.60000000000000142, 0.000000000000000000, 0.000000000000000000 ) ) ;
#5337=CARTESIAN_POINT ( 'NONE',  ( 3.958491816111018746, 1.406739583089935186, 3.500000000000000000 ) ) ;
#5362=CARTESIAN_POINT ( 'NONE',  ( 3.973110223767137850, 2.263269463293572928E-11, 3.565797985667434222 ) ) ;
#5388=DIRECTION ( 'NONE',  ( 0.000000000000000000, 0.000000000000000000, -1.000000000000000000 ) ) ;
#5433=CARTESIAN_POINT ( 'NONE',  ( -2.919722569185572480E-15, 2.859595677584338524, -2.047034997319574945 ) ) ;
#5438=ADVANCED_FACE ( 'NONE', ( #10599 ), #10408, .T. ) ;
#5485=CARTESIAN_POINT ( 'NONE',  ( -2.837560373301905643E-16, 0.3423821193871246504, -3.499999999999999556 ) ) ;
#5491=CARTESIAN_POINT ( 'NONE',  ( 0.3126073911696427010, 4.041451884327382338, -6.521455134176256610E-17 ) ) ;
#5503=CARTESIAN_POINT ( 'NONE',  ( 0.3126073911696451990, -4.041451884327386779, -1.834154111220703958E-17 ) ) ;
#5506=ORIENTED_EDGE ( 'NONE', *, *, #3836, .T. ) ;
#5520=CARTESIAN_POINT ( 'NONE',  ( 4.030875481282487627, 1.403567514399325367, 3.500000000000000000 ) ) ;
#5534=DIRECTION ( 'NONE',  ( -1.000000000000000000, -0.000000000000000000, -0.000000000000000000 ) ) ;
#5557=AXIS2_PLACEMENT_3D ( 'NONE', #19201, #17518, #16141 ) ;
#5559=EDGE_CURVE ( 'NONE', #19337, #9539, #2287, .T. ) ;
#5668=CARTESIAN_POINT ( 'NONE',  ( 0.000000000000000000, 3.755786496842903495E-16, 3.500000000000000000 ) ) ;
#5692=CARTESIAN_POINT ( 'NONE',  ( 4.124214193018069352, 2.028338413290941222, 3.513185186763553514 ) ) ;
#5696=CARTESIAN_POINT ( 'NONE',  ( 0.02993401039713615083, 3.373851915354614928, 1.156317065392238774 ) ) ;
#5701=CARTESIAN_POINT ( 'NONE',  ( 45.60000000000000142, 0.000000000000000000, 0.000000000000000000 ) ) ;
#5704=EDGE_CURVE ( 'NONE', #10511, #468, #9514, .T. ) ;
#5727=DIRECTION ( 'NONE',  ( 1.000000000000000000, 0.000000000000000000, -0.000000000000000000 ) ) ;
#5739=LINE ( 'NONE', #9840, #8846 ) ;
#5748=ORIENTED_EDGE ( 'NONE', *, *, #748, .F. ) ;
#5774=B_SPLINE_CURVE_WITH_KNOTS ( 'NONE', 3,
 ( #16956, #565, #9476, #6441, #17144, #3605 ),
 .UNSPECIFIED., .F., .F.,
 ( 4, 2, 4 ),
 ( 0.002044882221487524104, 0.003063384235218490244, 0.004081886248949456383 ),
 .UNSPECIFIED. ) ;
#5786=FACE_OUTER_BOUND ( 'NONE', #15131, .T. ) ;
#5800=EDGE_CURVE ( 'NONE', #3297, #4766, #17954, .T. ) ;
#5816=VERTEX_POINT ( 'NONE', #15796 ) ;
#5826=VERTEX_POINT ( 'NONE', #9994 ) ;
#5839=CARTESIAN_POINT ( 'NONE',  ( 5.599999999999999645, 4.041451884327382338, 0.000000000000000000 ) ) ;
#5855=ORIENTED_EDGE ( 'NONE', *, *, #14806, .T. ) ;
#5865=EDGE_CURVE ( 'NONE', #6937, #4747, #12261, .T. ) ;
#5869=ORIENTED_EDGE ( 'NONE', *, *, #15919, .F. ) ;
#5892=CARTESIAN_POINT ( 'NONE',  ( 3.951447005078450925, -2.357513599190971032, 2.916666666666666963 ) ) ;
#5987=CARTESIAN_POINT ( 'NONE',  ( 0.1388410611046082266, -2.351840044243035166, 2.926493552096024242 ) ) ;
#5990=PLANE ( 'NONE',  #13909 ) ;
#6001=CARTESIAN_POINT ( 'NONE',  ( 4.158921614371307030, 1.986121848748763741, -3.559936047944503912 ) ) ;
#6008=CARTESIAN_POINT ( 'NONE',  ( 4.050536630291688311, 2.401306687817038821, -2.976670123173768001 ) ) ;
#6038=PLANE ( 'NONE',  #1919 ) ;
#6042=ORIENTED_EDGE ( 'NONE', *, *, #6433, .F. ) ;
#6051=EDGE_CURVE ( 'NONE', #6699, #5816, #331, .T. ) ;
#6054=VERTEX_POINT ( 'NONE', #18253 ) ;
#6071=FILL_AREA_STYLE ('',( #6156 ) ) ;
#6089=CARTESIAN_POINT ( 'NONE',  ( 4.030867648405251025, 2.329326259789668452, -2.965488570640744115 ) ) ;
#6095=CARTESIAN_POINT ( 'NONE',  ( 6.897297840755645792E-16, -2.686816014504582739, -2.346298152288354366 ) ) ;
#6097=CARTESIAN_POINT ( 'NONE',  ( 0.000000000000000000, 0.000000000000000000, 0.000000000000000000 ) ) ;
#6106=CARTESIAN_POINT ( 'NONE',  ( 3.950241966888156320, -2.668221755853644073, -2.378504353000863158 ) ) ;
#6137=AXIS2_PLACEMENT_3D ( 'NONE', #11742, #8416, #5388 ) ;
#6156=FILL_AREA_STYLE_COLOUR ( '', #18458 ) ;
#6164=ORIENTED_EDGE ( 'NONE', *, *, #17255, .T. ) ;
#6165=ADVANCED_BREP_SHAPE_REPRESENTATION ( '', ( #8395, #10359 ), #10908 ) ;
#6179=EDGE_CURVE ( 'NONE', #13491, #17135, #12376, .T. ) ;
#6230=CONICAL_SURFACE ( 'NONE', #286, 3.500000000000000000, 1.047197551196600296 ) ;
#6252=SURFACE_STYLE_FILL_AREA ( #6071 ) ;
#6270=CONICAL_SURFACE ( 'NONE', #12521, 3.500000000000000000, 1.047197551196600296 ) ;
#6279=CARTESIAN_POINT ( 'NONE',  ( 4.175813232069147674, 2.061359961916367833, 3.570380186727398097 ) ) ;
#6284=CARTESIAN_POINT ( 'NONE',  ( 0.1217565302851044418, -2.351289329882175760, -2.927447417349501535 ) ) ;
#6373=DIRECTION ( 'NONE',  ( 0.000000000000000000, 0.000000000000000000, 1.000000000000000000 ) ) ;
#6378=EDGE_CURVE ( 'NONE', #5816, #16278, #8518, .T. ) ;
#6424=CARTESIAN_POINT ( 'NONE',  ( 4.180345136606690382, -2.085999704580137060, -3.570468642550115312 ) ) ;
#6433=EDGE_CURVE ( 'NONE', #6054, #14054, #11266, .T. ) ;
#6441=CARTESIAN_POINT ( 'NONE',  ( 0.1388410611046115850, -3.710337782248037009, -0.5735064479039788665 ) ) ;
#6464=PLANE ( 'NONE',  #17875 ) ;
#6469=B_SPLINE_CURVE_WITH_KNOTS ( 'NONE', 3,
 ( #9576, #2353, #675, #18725 ),
 .UNSPECIFIED., .F., .F.,
 ( 4, 4 ),
 ( 2.380739282169052541E-07, 0.002044882221487534079 ),
 .UNSPECIFIED. ) ;
#6486=ORIENTED_EDGE ( 'NONE', *, *, #8854, .T. ) ;
#6506=ORIENTED_EDGE ( 'NONE', *, *, #16708, .F. ) ;
#6510=FACE_OUTER_BOUND ( 'NONE', #11352, .T. ) ;
#6527=EDGE_LOOP ( 'NONE', ( #13958, #1667, #3186, #2118, #13628 ) ) ;
#6540=ORIENTED_EDGE ( 'NONE', *, *, #13415, .F. ) ;
#6550=CARTESIAN_POINT ( 'NONE',  ( 45.15499999999999403, 0.000000000000000000, 0.000000000000000000 ) ) ;
#6587=CARTESIAN_POINT ( 'NONE',  ( 4.151274195509685683, -2.039912954708743786, 3.533232880573501156 ) ) ;
#6595=LINE ( 'NONE', #5219, #470 ) ;
#6619=AXIS2_PLACEMENT_3D ( 'NONE', #9033, #17982, #7472 ) ;
#6646=B_SPLINE_CURVE_WITH_KNOTS ( 'NONE', 3,
 ( #8577, #5433, #14743, #11411, #18990, #17415 ),
 .UNSPECIFIED., .F., .F.,
 ( 4, 2, 4 ),
 ( 0.002044882221487534079, 0.003063384235218496315, 0.004081886248949458985 ),
 .UNSPECIFIED. ) ;
#6678=ADVANCED_FACE ( 'NONE', ( #6720 ), #349, .T. ) ;
#6697=CARTESIAN_POINT ( 'NONE',  ( 4.175813232069146785, 2.061359961916365613, -3.570380186727397653 ) ) ;
#6699=VERTEX_POINT ( 'NONE', #17330 ) ;
#6715=CARTESIAN_POINT ( 'NONE',  ( 4.158806965674306078, 1.986429158307092768, 3.559403772175832259 ) ) ;
#6720=FACE_OUTER_BOUND ( 'NONE', #13180, .T. ) ;
#6731=CARTESIAN_POINT ( 'NONE',  ( 0.000000000000000000, 0.000000000000000000, 0.000000000000000000 ) ) ;
#6732=EDGE_LOOP ( 'NONE', ( #9830, #7041, #13953, #13790 ) ) ;
#6763=EDGE_CURVE ( 'NONE', #4747, #6937, #9412, .T. ) ;
#6764=CARTESIAN_POINT ( 'NONE',  ( 0.000000000000000000, 3.755786496842903495E-16, 3.500000000000000000 ) ) ;
#6796=VERTEX_POINT ( 'NONE', #3104 ) ;
#6800=CARTESIAN_POINT ( 'NONE',  ( 3.950250160040163383, -0.7258013381021514165, 3.499999999999845013 ) ) ;
#6804=EDGE_CURVE ( 'NONE', #18672, #762, #8384, .T. ) ;
#6810=CARTESIAN_POINT ( 'NONE',  ( 3.950233766685291137, 0.7256672287179410930, -3.499999999999844125 ) ) ;
#6814=CARTESIAN_POINT ( 'NONE',  ( 4.165266963751723672, 2.049631966911992009, -3.550066703508905963 ) ) ;
#6824=EDGE_LOOP ( 'NONE', ( #10730, #11912, #6486, #4668, #2796 ) ) ;
#6854=CARTESIAN_POINT ( 'NONE',  ( 4.175326769692857987, 4.121399112977855772, 3.964526709274768569E-16 ) ) ;
#6856=CARTESIAN_POINT ( 'NONE',  ( 1.677125235563514178E-16, 0.3423821193476823121, 3.500000000000000444 ) ) ;
#6889=ADVANCED_FACE ( 'NONE', ( #1138 ), #6038, .F. ) ;
#6900=ORIENTED_EDGE ( 'NONE', *, *, #15393, .F. ) ;
#6907=CIRCLE ( 'NONE', #1592, 5.200000000000001066 ) ;
#6937=VERTEX_POINT ( 'NONE', #17626 ) ;
#6942=CARTESIAN_POINT ( 'NONE',  ( 4.071447262713887127, 2.020725942163686284, -3.499999999999999556 ) ) ;
#6956=ORIENTED_EDGE ( 'NONE', *, *, #9256, .T. ) ;
#7002=EDGE_LOOP ( 'NONE', ( #10993, #16054, #5506 ) ) ;
#7008=PLANE ( 'NONE',  #5557 ) ;
#7023=CARTESIAN_POINT ( 'NONE',  ( 4.175813232069146785, -2.061359961916366057, 3.570380186727398542 ) ) ;
#7037=CARTESIAN_POINT ( 'NONE',  ( 8.978549240895586059E-17, -0.3420925509381363971, 3.500000000000000444 ) ) ;
#7041=ORIENTED_EDGE ( 'NONE', *, *, #6051, .T. ) ;
#7045=DIRECTION ( 'NONE',  ( 1.000000000000000000, 0.000000000000000000, 0.000000000000000000 ) ) ;
#7110=CARTESIAN_POINT ( 'NONE',  ( 3.972709601346593455, -3.429395227388317036, -1.191688283765307110 ) ) ;
#7132=AXIS2_PLACEMENT_3D ( 'NONE', #13280, #5534, #14848 ) ;
#7149=ORIENTED_EDGE ( 'NONE', *, *, #8644, .F. ) ;
#7177=DIRECTION ( 'NONE',  ( -0.000000000000000000, 0.000000000000000000, 1.000000000000000000 ) ) ;
#7215=CARTESIAN_POINT ( 'NONE',  ( 0.000000000000000000, 3.031088913245533423, -1.750000000000004885 ) ) ;
#7222=VECTOR ( 'NONE', #4606, 1000.000000000000114 ) ;
#7223=CARTESIAN_POINT ( 'NONE',  ( 5.599999999999999645, -4.041451884327386779, 0.000000000000000000 ) ) ;
#7258=DIRECTION ( 'NONE',  ( 0.000000000000000000, -0.5000000000000012212, -0.8660254037844380415 ) ) ;
#7288=EDGE_CURVE ( 'NONE', #468, #19337, #13045, .T. ) ;
#7341=ORIENTED_EDGE ( 'NONE', *, *, #8447, .F. ) ;
#7343=ADVANCED_FACE ( 'NONE', ( #1582 ), #11293, .F. ) ;
#7358=CARTESIAN_POINT ( 'NONE',  ( 4.104070371397480876, -2.023683613428371775, -3.505122836902506922 ) ) ;
#7360=CARTESIAN_POINT ( 'NONE',  ( 3.974175853610027342, 3.450041667725633143, -1.156004144283977908 ) ) ;
#7366=VERTEX_POINT ( 'NONE', #10424 ) ;
#7380=CARTESIAN_POINT ( 'NONE',  ( 4.158806965674307854, -1.986429158307096321, -3.559403772175836256 ) ) ;
#7418=LINE ( 'NONE', #7223, #9392 ) ;
#7442=ORIENTED_EDGE ( 'NONE', *, *, #13415, .T. ) ;
#7446=CARTESIAN_POINT ( 'NONE',  ( 0.2174200650117537048, -2.185595227304857335, 3.214438021527933564 ) ) ;
#7456=CARTESIAN_POINT ( 'NONE',  ( 3.880206590543185730, 3.396506438958505125, -1.117078279489029935 ) ) ;
#7472=DIRECTION ( 'NONE',  ( 0.000000000000000000, 0.000000000000000000, 1.000000000000000000 ) ) ;
#7474=CARTESIAN_POINT ( 'NONE',  ( 3.878096787214417862, -3.381939201670079331, -1.142309474598505181 ) ) ;
#7505=VERTEX_POINT ( 'NONE', #15226 ) ;
#7529=VERTEX_POINT ( 'NONE', #14028 ) ;
#7546=DIRECTION ( 'NONE',  ( 0.000000000000000000, 0.000000000000000000, 1.000000000000000000 ) ) ;
#7608=CARTESIAN_POINT ( 'NONE',  ( 4.071447262713888016, 4.041451884327382338, 0.000000000000000000 ) ) ;
#7618=DIRECTION ( 'NONE',  ( 0.000000000000000000, 0.000000000000000000, 1.000000000000000000 ) ) ;
#7628=CARTESIAN_POINT ( 'NONE',  ( 0.3126073911696399255, 2.020725942163686284, -3.499999999999999556 ) ) ;
#7647=CARTESIAN_POINT ( 'NONE',  ( 4.086262629614029862, 4.082406995609985323, 0.07093633357110586124 ) ) ;
#7697=VECTOR ( 'NONE', #759, 1000.000000000000114 ) ;
#7709=ADVANCED_FACE ( 'NONE', ( #3370 ), #11408, .F. ) ;
#7733=EDGE_CURVE ( 'NONE', #5826, #13491, #17055, .T. ) ;
#7752=FACE_OUTER_BOUND ( 'NONE', #1222, .T. ) ;
#7754=AXIS2_PLACEMENT_3D ( 'NONE', #207, #3060, #15003 ) ;
#7793=CARTESIAN_POINT ( 'NONE',  ( 0.000000000000000000, 0.000000000000000000, 0.000000000000000000 ) ) ;
#7803=( LENGTH_UNIT ( ) NAMED_UNIT ( * ) SI_UNIT ( .MILLI., .METRE. ) );
#7812=ORIENTED_EDGE ( 'NONE', *, *, #306, .F. ) ;
#7860=CARTESIAN_POINT ( 'NONE',  ( 3.951447005078451813, 1.347150628109126558, 3.500000000000000444 ) ) ;
#7871=CARTESIAN_POINT ( 'NONE',  ( 4.082498951862918446, -2.020725942163685840, 3.500000000000002220 ) ) ;
#7879=EDGE_CURVE ( 'NONE', #7366, #2510, #14299, .T. ) ;
#7886=ORIENTED_EDGE ( 'NONE', *, *, #5800, .F. ) ;
#7902=CARTESIAN_POINT ( 'NONE',  ( 4.055492966679600464, 2.385006769472780785, 3.005124364834443451 ) ) ;
#7936=CARTESIAN_POINT ( 'NONE',  ( 4.175813232069146785, 2.061359961916365613, -3.570380186727397653 ) ) ;
#7975=ORIENTED_EDGE ( 'NONE', *, *, #16957, .F. ) ;
#8002=EDGE_CURVE ( 'NONE', #4766, #14054, #6469, .T. ) ;
#8028=EDGE_LOOP ( 'NONE', ( #386, #19403, #9426, #16669, #7812 ) ) ;
#8029=( BOUNDED_SURFACE ( )  B_SPLINE_SURFACE ( 3, 2, ( 
 ( #837, #12495, #546 ),
 ( #11216, #5055, #18411 ),
 ( #18698, #6810, #14253 ),
 ( #1936, #9550, #3498 ),
 ( #12798, #10927, #17032 ),
 ( #8083, #16835, #6424 ) ),
 .UNSPECIFIED., .F., .F., .F. ) 
 B_SPLINE_SURFACE_WITH_KNOTS ( ( 4, 2, 4 ),
 ( 3, 3 ),
 ( 0.01652267773200353021, 0.01858309280828997212, 0.02064350788457641403 ),
 ( 0.000000000000000000, 1.000000000000000000 ),
 .UNSPECIFIED. ) 
 GEOMETRIC_REPRESENTATION_ITEM ( )  RATIONAL_B_SPLINE_SURFACE ( (
 ( 1.000000000000000000, 0.8047780975688292315, 1.000000000000000000),
 ( 1.000000000000000000, 0.8123789546324570177, 1.000000000000000000),
 ( 1.000000000000000000, 0.8190677982988761041, 1.000000000000000000),
 ( 1.000000000000000000, 0.8192346069552172150, 1.000000000000000000),
 ( 1.000000000000000000, 0.8126126759768884655, 1.000000000000000000),
 ( 1.000000000000000000, 0.8047712639311999094, 1.000000000000000000) ) ) 
 REPRESENTATION_ITEM ( '' )  SURFACE ( )  );
#8069=ORIENTED_EDGE ( 'NONE', *, *, #15919, .T. ) ;
#8073=CARTESIAN_POINT ( 'NONE',  ( 4.086376210449952140, 2.103254844323300343, 3.500000000000000000 ) ) ;
#8083=CARTESIAN_POINT ( 'NONE',  ( 4.086375874528100027, -2.103253014742892280, -3.499999999999999556 ) ) ;
#8135=LINE ( 'NONE', #12354, #2345 ) ;
#8190=CARTESIAN_POINT ( 'NONE',  ( 4.071447262713890680, -4.041451884327386779, 0.000000000000000000 ) ) ;
#8230=CARTESIAN_POINT ( 'NONE',  ( 4.165266963751722784, 4.099263933823986683, 2.067493599750144616E-15 ) ) ;
#8266=CARTESIAN_POINT ( 'NONE',  ( 4.158806752148102248, -2.089318365061878513, 3.500000000000000000 ) ) ;
#8277=CARTESIAN_POINT ( 'NONE',  ( 4.030867648404937498, 3.732851566701761659, 0.5345114293584584120 ) ) ;
#8278=CARTESIAN_POINT ( 'NONE',  ( 4.114405500665258231, -4.051151509359434577, 3.301207616706364010E-16 ) ) ;
#8314=FACE_OUTER_BOUND ( 'NONE', #13167, .T. ) ;
#8325=CARTESIAN_POINT ( 'NONE',  ( 0.000000000000000000, 3.755786496842903495E-16, 3.500000000000000000 ) ) ;
#8345=ORIENTED_EDGE ( 'NONE', *, *, #17562, .T. ) ;
#8346=CARTESIAN_POINT ( 'NONE',  ( 4.033901012035946643, -3.740908793664254883, 0.5205559028926849408 ) ) ;
#8349=ADVANCED_FACE ( 'NONE', ( #17831 ), #16361, .T. ) ;
#8365=CARTESIAN_POINT ( 'NONE',  ( 4.052432342741587590, 1.393590342655181891, 3.567979436357439305 ) ) ;
#8378=CARTESIAN_POINT ( 'NONE',  ( 4.142654963991854622, -4.070796997468703715, 6.968404583626299416E-17 ) ) ;
#8384=B_SPLINE_CURVE_WITH_KNOTS ( 'NONE', 3,
 ( #4369, #4470, #7110, #4271, #10332, #13191 ),
 .UNSPECIFIED., .F., .F.,
 ( 4, 2, 4 ),
 ( 9.961792871202292917E-20, 0.002086519881787258883, 0.004173039763574517766 ),
 .UNSPECIFIED. ) ;
#8395=MANIFOLD_SOLID_BREP ( 'FlangeHexFillet', #3665 ) ;
#8399=EDGE_LOOP ( 'NONE', ( #7975, #17559, #3009, #12035, #8494 ) ) ;
#8410=CARTESIAN_POINT ( 'NONE',  ( 3.973514160553461849, 2.741076955031360285, 2.383932505289871884 ) ) ;
#8416=DIRECTION ( 'NONE',  ( 1.000000000000000000, 0.000000000000000000, -0.000000000000000000 ) ) ;
#8424=CARTESIAN_POINT ( 'NONE',  ( 4.071447262713888016, 4.041451884327382338, 0.000000000000000000 ) ) ;
#8447=EDGE_CURVE ( 'NONE', #18672, #468, #17869, .T. ) ;
#8452=CARTESIAN_POINT ( 'NONE',  ( 3.961551342853522950, -3.742715940867789026, 0.5174258321190450260 ) ) ;
#8488=AXIS2_PLACEMENT_3D ( 'NONE', #17522, #19300, #17813 ) ;
#8494=ORIENTED_EDGE ( 'NONE', *, *, #17938, .F. ) ;
#8496=DIRECTION ( 'NONE',  ( 0.000000000000000000, 0.000000000000000000, -1.000000000000000000 ) ) ;
#8501=CARTESIAN_POINT ( 'NONE',  ( 4.175813232069147674, 2.061359961916367833, 3.570380186727398097 ) ) ;
#8518=LINE ( 'NONE', #14489, #1899 ) ;
#8528=ORIENTED_EDGE ( 'NONE', *, *, #9882, .F. ) ;
#8530=CARTESIAN_POINT ( 'NONE',  ( 4.124214193018070240, 4.056676826581888662, 1.068854115921270076E-15 ) ) ;
#8577=CARTESIAN_POINT ( 'NONE',  ( 0.000000000000000000, 3.031088913245533423, -1.750000000000004885 ) ) ;
#8592=CARTESIAN_POINT ( 'NONE',  ( 3.973110223768738791, 0.6864646529411682074, 3.565797985667475967 ) ) ;
#8605=ADVANCED_FACE ( 'NONE', ( #2530 ), #7008, .F. ) ;
#8612=CARTESIAN_POINT ( 'NONE',  ( 4.175813232069148562, 4.122719923832741884, -2.765695189283172261E-17 ) ) ;
#8630=CARTESIAN_POINT ( 'NONE',  ( 4.175572532730932096, -2.061029303918058275, -3.569807470274390493 ) ) ;
#8644=EDGE_CURVE ( 'NONE', #5816, #6699, #4634, .T. ) ;
#8667=B_SPLINE_CURVE_WITH_KNOTS ( 'NONE', 3,
 ( #18403, #15533, #9350, #13581, #17024, #443 ),
 .UNSPECIFIED., .F., .F.,
 ( 4, 2, 4 ),
 ( 0.000000000000000000, 0.002086519881787261485, 0.004173039763574522970 ),
 .UNSPECIFIED. ) ;
#8669=AXIS2_PLACEMENT_3D ( 'NONE', #1785, #593, #18174 ) ;
#8831=CARTESIAN_POINT ( 'NONE',  ( 3.958484000407829217, 2.327740518749080056, -2.968235154689852440 ) ) ;
#8834=DIRECTION ( 'NONE',  ( 0.000000000000000000, 0.000000000000000000, 1.000000000000000000 ) ) ;
#8846=VECTOR ( 'NONE', #2425, 1000.000000000000000 ) ;
#8849=CARTESIAN_POINT ( 'NONE',  ( 3.880206590543187950, -2.665671387532591474, -2.382921720510934538 ) ) ;
#8854=EDGE_CURVE ( 'NONE', #9539, #14839, #6595, .T. ) ;
#8871=CARTESIAN_POINT ( 'NONE',  ( 0.000000000000000000, 4.041451884327382338, 0.000000000000000000 ) ) ;
#8885=ORIENTED_EDGE ( 'NONE', *, *, #6804, .T. ) ;
#8892=EDGE_CURVE ( 'NONE', #7505, #7366, #3606, .T. ) ;
#8923=CARTESIAN_POINT ( 'NONE',  ( 4.158806965674307854, 4.075748668183981849, 0.05940377217583739378 ) ) ;
#8934=CARTESIAN_POINT ( 'NONE',  ( 0.000000000000000000, -3.031088913245531202, 1.750000000000006439 ) ) ;
#8948=DIRECTION ( 'NONE',  ( 0.000000000000000000, 0.000000000000000000, -1.000000000000000000 ) ) ;
#8952=ORIENTED_EDGE ( 'NONE', *, *, #669, .T. ) ;
#8967=B_SPLINE_CURVE_WITH_KNOTS ( 'NONE', 3,
 ( #5503, #16402, #11477, #8934 ),
 .UNSPECIFIED., .F., .F.,
 ( 4, 4 ),
 ( 2.380739282168708963E-07, 0.002044882221487539717 ),
 .UNSPECIFIED. ) ;
#8987=DIRECTION ( 'NONE',  ( 0.000000000000000000, 0.000000000000000000, -1.000000000000000000 ) ) ;
#9028=CARTESIAN_POINT ( 'NONE',  ( 0.000000000000000000, 0.000000000000000000, 0.000000000000000000 ) ) ;
#9033=CARTESIAN_POINT ( 'NONE',  ( 0.000000000000000000, 0.000000000000000000, 0.000000000000000000 ) ) ;
#9074=ORIENTED_EDGE ( 'NONE', *, *, #6378, .F. ) ;
#9089=DIRECTION ( 'NONE',  ( 0.000000000000000000, 0.000000000000000000, -1.000000000000000000 ) ) ;
#9108=DIRECTION ( 'NONE',  ( -1.000000000000000000, -0.000000000000000000, -0.000000000000000000 ) ) ;
#9120=CARTESIAN_POINT ( 'NONE',  ( 3.972066048304756514, 2.740530939476224059, -2.384802634787894338 ) ) ;
#9171=FACE_OUTER_BOUND ( 'NONE', #14834, .T. ) ;
#9189=EDGE_LOOP ( 'NONE', ( #5748, #2366, #16817, #17111 ) ) ;
#9242=B_SPLINE_CURVE_WITH_KNOTS ( 'NONE', 3,
 ( #13750, #7871, #12370, #17293, #18669, #713, #9523, #807, #6587, #15512, #3556, #12666, #9908, #15810, #5211, #3653 ),
 .UNSPECIFIED., .F., .F.,
 ( 4, 3, 3, 3, 3, 4 ),
 ( 0.000000000000000000, 3.315506744709513341E-05, 6.608280158699547874E-05, 0.0001026520855291439131, 0.0001376952025664790686, 0.0001398064759190603148 ),
 .UNSPECIFIED. ) ;
#9256=EDGE_CURVE ( 'NONE', #14216, #9274, #19269, .T. ) ;
#9274=VERTEX_POINT ( 'NONE', #1688 ) ;
#9278=PRESENTATION_STYLE_ASSIGNMENT (( #12322 ) ) ;
#9329=CARTESIAN_POINT ( 'NONE',  ( 0.000000000000000000, 0.000000000000000000, -3.499999999999999556 ) ) ;
#9341=MECHANICAL_DESIGN_GEOMETRIC_PRESENTATION_REPRESENTATION('',(#9970),#4665);
#9350=CARTESIAN_POINT ( 'NONE',  ( 3.972709601346592123, -2.746729940827190575, 2.374099244652734697 ) ) ;
#9356=ORIENTED_EDGE ( 'NONE', *, *, #16139, .T. ) ;
#9360=CARTESIAN_POINT ( 'NONE',  ( 4.151274195509685683, 2.039912954708744230, -3.533232880573500267 ) ) ;
#9387=AXIS2_PLACEMENT_3D ( 'NONE', #5839, #1527, #13285 ) ;
#9392=VECTOR ( 'NONE', #10249, 1000.000000000000000 ) ;
#9396=AXIS2_PLACEMENT_3D ( 'NONE', #6550, #10772, #14090 ) ;
#9412=CIRCLE ( 'NONE', #8488, 2.055000000000000160 ) ;
#9426=ORIENTED_EDGE ( 'NONE', *, *, #5015, .T. ) ;
#9463=CARTESIAN_POINT ( 'NONE',  ( 4.158921614371307918, 4.076055977742304215, -0.05993604794450364120 ) ) ;
#9476=CARTESIAN_POINT ( 'NONE',  ( 0.02993401039713891598, -3.373851915354620257, -1.156317065392238774 ) ) ;
#9483=DIRECTION ( 'NONE',  ( 0.000000000000000000, 0.000000000000000000, 1.000000000000000000 ) ) ;
#9500=UNCERTAINTY_MEASURE_WITH_UNIT (LENGTH_MEASURE( 1.000000000000000082E-05 ), #7803, 'distance_accuracy_value', 'NONE');
#9514=B_SPLINE_CURVE_WITH_KNOTS ( 'NONE', 3,
 ( #11561, #3839, #19151, #15894, #9894 ),
 .UNSPECIFIED., .F., .F.,
 ( 4, 1, 4 ),
 ( 0.000000000000000000, 0.002020725942163690506, 0.004041451884327381013 ),
 .UNSPECIFIED. ) ;
#9523=CARTESIAN_POINT ( 'NONE',  ( 4.132952817037866211, -2.031684012687259511, 3.518979934899751250 ) ) ;
#9539=VERTEX_POINT ( 'NONE', #18735 ) ;
#9543=CARTESIAN_POINT ( 'NONE',  ( 4.071447262713888016, -2.020725942163694722, -3.499999999999999556 ) ) ;
#9550=CARTESIAN_POINT ( 'NONE',  ( 3.948111298835276894, -0.6968132764964354298, -3.500000000000154987 ) ) ;
#9554=CARTESIAN_POINT ( 'NONE',  ( 4.170895651974851681, -4.109780709045220526, -1.251026243406537913E-13 ) ) ;
#9576=CARTESIAN_POINT ( 'NONE',  ( 0.3126073911696427010, 4.041451884327382338, -6.521455134176256610E-17 ) ) ;
#9615=EDGE_CURVE ( 'NONE', #5826, #9274, #11444, .T. ) ;
#9699=CARTESIAN_POINT ( 'NONE',  ( 4.165266963751721896, 2.049631966911991565, 3.550066703508901078 ) ) ;
#9702=CARTESIAN_POINT ( 'NONE',  ( 4.071447262713887127, -2.020725942163686284, 3.500000000000000444 ) ) ;
#9723=DIRECTION ( 'NONE',  ( -0.000000000000000000, 1.000000000000000000, 1.224646799147353207E-16 ) ) ;
#9752=CARTESIAN_POINT ( 'NONE',  ( 3.950241966888466738, 2.668221755853590782, 2.378504353001025695 ) ) ;
#9798=CARTESIAN_POINT ( 'NONE',  ( 4.132952817037859994, 2.031684012687258623, 3.518979934899746809 ) ) ;
#9806=ORIENTED_EDGE ( 'NONE', *, *, #17782, .T. ) ;
#9814=CARTESIAN_POINT ( 'NONE',  ( 4.055492966679659084, -3.795017426214758682, 0.5629142681442622642 ) ) ;
#9830=ORIENTED_EDGE ( 'NONE', *, *, #2105, .F. ) ;
#9837=CIRCLE ( 'NONE', #3600, 5.200000000000001066 ) ;
#9840=CARTESIAN_POINT ( 'NONE',  ( 45.60000000000000142, 2.516649172247811061E-16, -2.055000000000000160 ) ) ;
#9882=EDGE_CURVE ( 'NONE', #9274, #3703, #5774, .T. ) ;
#9889=CARTESIAN_POINT ( 'NONE',  ( 4.142654963991853734, 4.070796997468700162, 1.458723597913840680E-15 ) ) ;
#9892=CARTESIAN_POINT ( 'NONE',  ( 4.142654963991853734, 2.035398498734346973, 3.525413613457309747 ) ) ;
#9894=CARTESIAN_POINT ( 'NONE',  ( 4.071447262713890680, -4.041451884327386779, 0.000000000000000000 ) ) ;
#9897=DIRECTION ( 'NONE',  ( 0.000000000000000000, 0.000000000000000000, 1.000000000000000000 ) ) ;
#9908=CARTESIAN_POINT ( 'NONE',  ( 4.175075985190095373, -2.060370777630118777, 3.568666869285566090 ) ) ;
#9911=CARTESIAN_POINT ( 'NONE',  ( 3.974175853610083742, -3.450041667725777472, 1.156004144284040303 ) ) ;
#9929=CARTESIAN_POINT ( 'NONE',  ( 4.180231680468789790, -2.085385483809538698, 3.570466434508605680 ) ) ;
#9970=STYLED_ITEM ( 'NONE', ( #9278 ), #6165 ) ;
#9976=EDGE_CURVE ( 'NONE', #1555, #2510, #12329, .T. ) ;
#9982=ADVANCED_FACE ( 'NONE', ( #4973 ), #12381, .T. ) ;
#9987=CARTESIAN_POINT ( 'NONE',  ( 0.03027795056225670092, 0.6888063905605149584, -3.499999999999999556 ) ) ;
#9994=CARTESIAN_POINT ( 'NONE',  ( 0.000000000000000000, -3.031088913245531202, 1.750000000000006439 ) ) ;
#10021=CARTESIAN_POINT ( 'NONE',  ( 4.071447262713890680, -4.041451884327386779, 0.000000000000000000 ) ) ;
#10072=CARTESIAN_POINT ( 'NONE',  ( 45.60000000000000142, 0.000000000000000000, 2.055000000000000160 ) ) ;
#10080=( LENGTH_UNIT ( ) NAMED_UNIT ( * ) SI_UNIT ( .MILLI., .METRE. ) );
#10081=DIRECTION ( 'NONE',  ( 0.000000000000000000, 0.000000000000000000, -1.000000000000000000 ) ) ;
#10091=CARTESIAN_POINT ( 'NONE',  ( 4.158413352280809328, 4.089743253945647972, 1.634918261399485461E-15 ) ) ;
#10094=CARTESIAN_POINT ( 'NONE',  ( 4.158413352280808439, 2.044871626972822209, 3.541821552872961298 ) ) ;
#10096=CARTESIAN_POINT ( 'NONE',  ( -1.959187206999195895E-15, 3.202582148906728765, 1.452965002680430828 ) ) ;
#10099=CARTESIAN_POINT ( 'NONE',  ( 4.175075985190096262, -2.060370777630117889, -3.568666869285569643 ) ) ;
#10142=DIRECTION ( 'NONE',  ( 1.000000000000000000, 0.000000000000000000, -0.000000000000000000 ) ) ;
#10170=ORIENTED_EDGE ( 'NONE', *, *, #9882, .T. ) ;
#10238=STYLED_ITEM('',(#19475),#8395);
#10249=DIRECTION ( 'NONE',  ( -1.000000000000000000, -0.000000000000000000, -0.000000000000000000 ) ) ;
#10261=DIRECTION ( 'NONE',  ( 1.000000000000000000, 0.000000000000000000, -0.000000000000000000 ) ) ;
#10290=CARTESIAN_POINT ( 'NONE',  ( 4.071447262713888016, -2.020725942163694722, -3.499999999999999556 ) ) ;
#10308=CARTESIAN_POINT ( 'NONE',  ( 3.958484000407238579, -3.734437307742088485, -0.5317648453099828032 ) ) ;
#10332=CARTESIAN_POINT ( 'NONE',  ( 4.050823680195224874, -2.400527758044906701, -2.978030508226146900 ) ) ;
#10341=ORIENTED_EDGE ( 'NONE', *, *, #184, .F. ) ;
#10352=CARTESIAN_POINT ( 'NONE',  ( 4.175813232069148562, 4.122719923832741884, -2.765695189283172261E-17 ) ) ;
#10359=AXIS2_PLACEMENT_3D ( 'NONE', #2871, #8834, #16191 ) ;
#10371=CARTESIAN_POINT ( 'NONE',  ( 0.3126073911696407026, -2.020725942163686728, 3.500000000000000444 ) ) ;
#10391=B_SPLINE_CURVE_WITH_KNOTS ( 'NONE', 3,
 ( #9329, #12179, #15413, #15221, #18377, #16706 ),
 .UNSPECIFIED., .F., .F.,
 ( 4, 2, 4 ),
 ( 0.01308430720669670130, 0.01410661709916351952, 0.01512892699163033601 ),
 .UNSPECIFIED. ) ;
#10408=CYLINDRICAL_SURFACE ( 'NONE', #6619, 2.500000000000000444 ) ;
#10424=CARTESIAN_POINT ( 'NONE',  ( 4.630153689607048761, 0.000000000000000000, -5.371010071662833063 ) ) ;
#10473=PRODUCT_DEFINITION_CONTEXT ( 'detailed design', #14660, 'design' ) ;
#10503=ADVANCED_FACE ( 'NONE', ( #6510 ), #15993, .T. ) ;
#10511=VERTEX_POINT ( 'NONE', #9543 ) ;
#10548=CARTESIAN_POINT ( 'NONE',  ( 4.071447262713887127, 2.020725942163686284, -3.499999999999999556 ) ) ;
#10551=ORIENTED_EDGE ( 'NONE', *, *, #1783, .T. ) ;
#10598=B_SPLINE_CURVE_WITH_KNOTS ( 'NONE', 3,
 ( #11489, #11302, #14337, #6697 ),
 .UNSPECIFIED., .F., .F.,
 ( 4, 4 ),
 ( 0.002080789711329296236, 0.004173039763574516031 ),
 .UNSPECIFIED. ) ;
#10599=FACE_OUTER_BOUND ( 'NONE', #6732, .T. ) ;
#10628=B_SPLINE_CURVE_WITH_KNOTS ( 'NONE', 3,
 ( #18415, #549, #14256, #12698, #18701, #6814, #18800, #9360, #15354, #646, #3500, #1939, #4956, #17034, #13873, #455 ),
 .UNSPECIFIED., .F., .F.,
 ( 4, 3, 3, 3, 3, 4 ),
 ( -2.111273352581767125E-06, 0.000000000000000000, 3.519286887793215919E-05, 7.191842652067064129E-05, 0.0001049868727093590168, 0.0001382836236822123786 ),
 .UNSPECIFIED. ) ;
#10663=ORIENTED_EDGE ( 'NONE', *, *, #13576, .F. ) ;
#10687=ORIENTED_EDGE ( 'NONE', *, *, #5559, .F. ) ;
#10701=CARTESIAN_POINT ( 'NONE',  ( 3.974175853610014908, -2.726149789692841274, -2.409821656223155806 ) ) ;
#10730=ORIENTED_EDGE ( 'NONE', *, *, #14539, .F. ) ;
#10754=( NAMED_UNIT ( * ) SI_UNIT ( $, .STERADIAN. ) SOLID_ANGLE_UNIT ( ) );
#10772=DIRECTION ( 'NONE',  ( -1.000000000000000000, -0.000000000000000000, -0.000000000000000000 ) ) ;
#10846=( LENGTH_UNIT ( ) NAMED_UNIT ( * ) SI_UNIT ( .MILLI., .METRE. ) );
#10873=APPLICATION_CONTEXT ( 'automotive_design' ) ;
#10905=CARTESIAN_POINT ( 'NONE',  ( 3.973110223768737015, -0.6864646529411583264, -3.565797985667475078 ) ) ;
#10908=( GEOMETRIC_REPRESENTATION_CONTEXT ( 3 ) GLOBAL_UNCERTAINTY_ASSIGNED_CONTEXT ( ( #12049 ) ) GLOBAL_UNIT_ASSIGNED_CONTEXT ( ( #10080, #275, #1561 ) ) REPRESENTATION_CONTEXT ( 'NONE', 'WORKASPACE' ) );
#10920=DIRECTION ( 'NONE',  ( 0.000000000000000000, 0.000000000000000000, -1.000000000000000000 ) ) ;
#10927=CARTESIAN_POINT ( 'NONE',  ( 4.030859730899086557, -1.403482646610860307, -3.500000000000000000 ) ) ;
#10930=CARTESIAN_POINT ( 'NONE',  ( 4.158413352280810216, -4.089743253945651524, 4.401844587977598791E-16 ) ) ;
#10993=ORIENTED_EDGE ( 'NONE', *, *, #5800, .T. ) ;
#11003=B_SPLINE_CURVE_WITH_KNOTS ( 'NONE', 3,
 ( #8501, #755, #8592, #5362 ),
 .UNSPECIFIED., .F., .F.,
 ( 4, 4 ),
 ( 0.000000000000000000, 0.002080789711329271950 ),
 .UNSPECIFIED. ) ;
#11068=CARTESIAN_POINT ( 'NONE',  ( 5.599999999999999645, 4.041451884327382338, 0.000000000000000000 ) ) ;
#11069=EDGE_LOOP ( 'NONE', ( #131, #6164, #2853, #1366 ) ) ;
#11096=DIRECTION ( 'NONE',  ( 0.000000000000000000, -1.000000000000000000, 0.000000000000000000 ) ) ;
#11113=ORIENTED_EDGE ( 'NONE', *, *, #306, .T. ) ;
#11121=CARTESIAN_POINT ( 'NONE',  ( 4.033901012036116285, 2.321269032827693035, 2.979444097106929146 ) ) ;
#11122=CARTESIAN_POINT ( 'NONE',  ( 4.175075985190098926, -4.120741555260250877, 2.761631486132788719E-14 ) ) ;
#11148=PRODUCT ( 'hex flange bolt small_iso_ISO 4162 - M5 x 40 x 16-N', 'hex flange bolt small_iso_ISO 4162 - M5 x 40 x 16-N', '', ( #14606 ) ) ;
#11191=CARTESIAN_POINT ( 'NONE',  ( 5.100000000000002309, 6.368163355566238354E-16, -5.200000000000001066 ) ) ;
#11216=CARTESIAN_POINT ( 'NONE',  ( 3.961545574370306966, 1.423222908132971476, -3.499999999999999556 ) ) ;
#11218=CARTESIAN_POINT ( 'NONE',  ( 4.086262629614028086, 1.979770830881088850, 3.570936333571100629 ) ) ;
#11235=VERTEX_POINT ( 'NONE', #1347 ) ;
#11241=AXIS2_PLACEMENT_3D ( 'NONE', #18596, #3670, #11398 ) ;
#11266=CIRCLE ( 'NONE', #15356, 3.500000000000000000 ) ;
#11273=DIRECTION ( 'NONE',  ( -1.000000000000000000, -0.000000000000000000, -0.000000000000000000 ) ) ;
#11281=AXIS2_PLACEMENT_3D ( 'NONE', #2630, #12805, #1047 ) ;
#11290=CARTESIAN_POINT ( 'NONE',  ( 0.3126073911696451990, -4.041451884327386779, -1.834154111220703958E-17 ) ) ;
#11293=( BOUNDED_SURFACE ( )  B_SPLINE_SURFACE ( 3, 2, ( 
 ( #7647, #8923, #3059 ),
 ( #110, #3154, #15106 ),
 ( #7456, #2960, #7360 ),
 ( #4526, #13437, #9120 ),
 ( #8831, #6089, #1683 ),
 ( #1384, #6001, #18059 ) ),
 .UNSPECIFIED., .F., .F., .F. ) 
 B_SPLINE_SURFACE_WITH_KNOTS ( ( 4, 2, 4 ),
 ( 3, 3 ),
 ( 0.01651999345535503164, 0.01858032176739832925, 0.02064065007944162339 ),
 ( 0.000000000000000000, 1.000000000000000000 ),
 .UNSPECIFIED. ) 
 GEOMETRIC_REPRESENTATION_ITEM ( )  RATIONAL_B_SPLINE_SURFACE ( (
 ( 1.000000000000000000, 0.8047781103519391355, 1.000000000000000000),
 ( 1.000000000000000000, 0.8123785825612301892, 1.000000000000000000),
 ( 1.000000000000000000, 0.8190671539777686361, 1.000000000000000000),
 ( 1.000000000000000000, 0.8192352254845479687, 1.000000000000000000),
 ( 1.000000000000000000, 0.8126129677203643986, 1.000000000000000000),
 ( 1.000000000000000000, 0.8047712537969725632, 1.000000000000000000) ) ) 
 REPRESENTATION_ITEM ( '' )  SURFACE ( )  );
#11302=CARTESIAN_POINT ( 'NONE',  ( 3.973110223765528914, 0.6902454861566579281, -3.565797985667391146 ) ) ;
#11310=CARTESIAN_POINT ( 'NONE',  ( 3.974183935050568106, -0.7239581970520293508, 3.565826011443134824 ) ) ;
#11321=CARTESIAN_POINT ( 'NONE',  ( 4.180231891692618440, 2.049421325483208101, 3.591231015387272851 ) ) ;
#11352=EDGE_LOOP ( 'NONE', ( #6956, #3865, #9356 ) ) ;
#11398=DIRECTION ( 'NONE',  ( 1.000000000000000000, 0.000000000000000000, 0.000000000000000000 ) ) ;
#11400=CARTESIAN_POINT ( 'NONE',  ( 4.086262418390198548, -2.102635014057361751, 3.500000000000000444 ) ) ;
#11408=( BOUNDED_SURFACE ( )  B_SPLINE_SURFACE ( 3, 2, ( 
 ( #15327, #1906, #2495 ),
 ( #8452, #8346, #9814 ),
 ( #19238, #3951, #9911 ),
 ( #4415, #15813, #4 ),
 ( #14432, #3045, #14326 ),
 ( #14992, #5315, #908 ) ),
 .UNSPECIFIED., .F., .F., .F. ) 
 B_SPLINE_SURFACE_WITH_KNOTS ( ( 4, 2, 4 ),
 ( 3, 3 ),
 ( 0.01651999345535504551, 0.01858032176739835006, 0.02064065007944165114 ),
 ( 0.000000000000000000, 1.000000000000000000 ),
 .UNSPECIFIED. ) 
 GEOMETRIC_REPRESENTATION_ITEM ( )  RATIONAL_B_SPLINE_SURFACE ( (
 ( 1.000000000000000000, 0.8047781103519391355, 1.000000000000000000),
 ( 1.000000000000000000, 0.8123785825613523137, 1.000000000000000000),
 ( 1.000000000000000000, 0.8190671539776074317, 1.000000000000000000),
 ( 1.000000000000000000, 0.8192352254847047321, 1.000000000000000000),
 ( 1.000000000000000000, 0.8126129677202470480, 1.000000000000000000),
 ( 1.000000000000000000, 0.8047712537969722302, 1.000000000000000000) ) ) 
 REPRESENTATION_ITEM ( '' )  SURFACE ( )  );
#11411=CARTESIAN_POINT ( 'NONE',  ( 0.1388410611046073107, 2.351840044243033834, -2.926493552096022022 ) ) ;
#11422=PLANE ( 'NONE',  #9387 ) ;
#11423=VERTEX_POINT ( 'NONE', #10352 ) ;
#11444=CIRCLE ( 'NONE', #6137, 3.500000000000000000 ) ;
#11451=ORIENTED_EDGE ( 'NONE', *, *, #17782, .F. ) ;
#11456=CARTESIAN_POINT ( 'NONE',  ( 0.1397371499201710277, 1.362866705336852169, -3.500000000000000000 ) ) ;
#11459=CARTESIAN_POINT ( 'NONE',  ( 4.175326769692855322, 2.060699556488906126, 3.569236330973482030 ) ) ;
#11477=CARTESIAN_POINT ( 'NONE',  ( -1.438549683741723797E-15, -3.375361811986503202, 1.153701847711634532 ) ) ;
#11481=LINE ( 'NONE', #11682, #14005 ) ;
#11489=CARTESIAN_POINT ( 'NONE',  ( 3.973110223767137850, -2.261493176400255405E-11, -3.565797985667433334 ) ) ;
#11518=CARTESIAN_POINT ( 'NONE',  ( 0.3126073911696408136, 2.020725942163688060, 3.500000000000000000 ) ) ;
#11524=EDGE_LOOP ( 'NONE', ( #8952, #10663, #14081, #6506 ) ) ;
#11540=CARTESIAN_POINT ( 'NONE',  ( 0.02944718078426972890, -0.6813962075686093023, 3.500000000000000000 ) ) ;
#11545=ORIENTED_EDGE ( 'NONE', *, *, #1847, .T. ) ;
#11561=CARTESIAN_POINT ( 'NONE',  ( 4.071447262713888016, -2.020725942163694722, -3.499999999999999556 ) ) ;
#11580=ORIENTED_EDGE ( 'NONE', *, *, #5865, .F. ) ;
#11621=ORIENTED_EDGE ( 'NONE', *, *, #13030, .F. ) ;
#11629=DIRECTION ( 'NONE',  ( 0.000000000000000000, 0.5000000000000007772, -0.8660254037844381525 ) ) ;
#11644=CARTESIAN_POINT ( 'NONE',  ( 3.951447005078450037, 2.357513599190969256, -2.916666666666667407 ) ) ;
#11647=DIRECTION ( 'NONE',  ( 0.000000000000000000, 0.000000000000000000, 1.000000000000000000 ) ) ;
#11682=CARTESIAN_POINT ( 'NONE',  ( 5.599999999999999645, 2.020725942163686284, -3.499999999999999556 ) ) ;
#11730=CARTESIAN_POINT ( 'NONE',  ( 3.951447005078448260, 1.347150628109122339, -3.499999999999999112 ) ) ;
#11732=CONICAL_SURFACE ( 'NONE', #16765, 2.055000000000000160, 0.7853981633974400633 ) ;
#11735=ORIENTED_EDGE ( 'NONE', *, *, #2105, .T. ) ;
#11742=CARTESIAN_POINT ( 'NONE',  ( 0.000000000000000000, 0.000000000000000000, 0.000000000000000000 ) ) ;
#11833=EDGE_LOOP ( 'NONE', ( #4789, #11580 ) ) ;
#11845=ORIENTED_EDGE ( 'NONE', *, *, #17562, .F. ) ;
#11912=ORIENTED_EDGE ( 'NONE', *, *, #5559, .T. ) ;
#12027=CARTESIAN_POINT ( 'NONE',  ( 3.806834918298644066, -4.553649124439118623E-15, -3.499999999999999556 ) ) ;
#12035=ORIENTED_EDGE ( 'NONE', *, *, #7733, .F. ) ;
#12049=UNCERTAINTY_MEASURE_WITH_UNIT (LENGTH_MEASURE( 1.000000000000000082E-05 ), #10080, 'distance_accuracy_value', 'NONE');
#12070=CARTESIAN_POINT ( 'NONE',  ( 4.630153689607048761, 0.000000000000000000, 0.000000000000000000 ) ) ;
#12134=AXIS2_PLACEMENT_3D ( 'NONE', #2927, #12218, #7618 ) ;
#12165=CARTESIAN_POINT ( 'NONE',  ( 0.3126073911696399255, 2.020725942163686284, -3.499999999999999556 ) ) ;
#12179=CARTESIAN_POINT ( 'NONE',  ( -2.134523027080836115E-16, -0.3420925509533478404, -3.499999999999999112 ) ) ;
#12218=DIRECTION ( 'NONE',  ( -1.000000000000000000, -0.000000000000000000, -0.000000000000000000 ) ) ;
#12229=( NAMED_UNIT ( * ) PLANE_ANGLE_UNIT ( ) SI_UNIT ( $, .RADIAN. ) );
#12261=CIRCLE ( 'NONE', #3819, 2.055000000000000160 ) ;
#12296=CARTESIAN_POINT ( 'NONE',  ( 4.175813232069150338, -4.122719923832746325, 2.362127131240695889E-16 ) ) ;
#12312=CARTESIAN_POINT ( 'NONE',  ( 5.599999999999999645, 3.061616997868383634E-16, -2.500000000000000444 ) ) ;
#12322=SURFACE_STYLE_USAGE ( .BOTH. , #13793 ) ;
#12329=LINE ( 'NONE', #18430, #7697 ) ;
#12346=CARTESIAN_POINT ( 'NONE',  ( 5.599999999999999645, 4.041451884327382338, 0.000000000000000000 ) ) ;
#12354=CARTESIAN_POINT ( 'NONE',  ( 45.60000000000000142, 0.000000000000000000, 2.055000000000000160 ) ) ;
#12370=CARTESIAN_POINT ( 'NONE',  ( 4.093692494532773729, -2.021783646005766766, 3.501831996793844493 ) ) ;
#12376=B_SPLINE_CURVE_WITH_KNOTS ( 'NONE', 3,
 ( #18728, #18833, #18927, #11540, #7037, #5668 ),
 .UNSPECIFIED., .F., .F.,
 ( 4, 2, 4 ),
 ( 0.003805861006858101119, 0.004828937052660003254, 0.005852013098461904955 ),
 .UNSPECIFIED. ) ;
#12381=CONICAL_SURFACE ( 'NONE', #13648, 3.500000000000000000, 1.047197551196600296 ) ;
#12490=ORIENTED_EDGE ( 'NONE', *, *, #8644, .T. ) ;
#12495=CARTESIAN_POINT ( 'NONE',  ( 4.158807179406255550, 2.089320655794525639, -3.500000000000000000 ) ) ;
#12498=FACE_OUTER_BOUND ( 'NONE', #17916, .T. ) ;
#12503=CONICAL_SURFACE ( 'NONE', #2514, 3.500000000000000000, 1.047197551196600296 ) ;
#12506=B_SPLINE_CURVE_WITH_KNOTS ( 'NONE', 3,
 ( #8424, #15984, #14305, #18654, #12840, #8530, #18848, #9889, #988, #10091, #8230, #12745, #16086, #6854, #792, #15888 ),
 .UNSPECIFIED., .F., .F.,
 ( 4, 3, 3, 3, 3, 4 ),
 ( 0.000000000000000000, 3.315506744709155554E-05, 6.608280158698769959E-05, 0.0001026520855291340739, 0.0001376952025664813454, 0.0001398064759190616429 ),
 .UNSPECIFIED. ) ;
#12521=AXIS2_PLACEMENT_3D ( 'NONE', #6097, #312, #13730 ) ;
#12533=LINE ( 'NONE', #293, #2392 ) ;
#12553=FACE_OUTER_BOUND ( 'NONE', #9189, .T. ) ;
#12563=ADVANCED_FACE ( 'NONE', ( #8314 ), #13699, .T. ) ;
#12666=CARTESIAN_POINT ( 'NONE',  ( 4.170895651974849905, -2.054890354522598273, 3.559174498016383748 ) ) ;
#12698=CARTESIAN_POINT ( 'NONE',  ( 4.175075985190094485, 2.060370777630093464, -3.568666869285578080 ) ) ;
#12715=DIRECTION ( 'NONE',  ( 0.000000000000000000, 0.000000000000000000, -1.000000000000000000 ) ) ;
#12744=ADVANCED_FACE ( 'NONE', ( #4919 ), #13394, .T. ) ;
#12745=CARTESIAN_POINT ( 'NONE',  ( 4.170895651974850793, 4.109780709045216085, 3.964526709274768569E-16 ) ) ;
#12798=CARTESIAN_POINT ( 'NONE',  ( 3.958476099524539382, -1.406653531810738933, -3.499999999999999556 ) ) ;
#12801=CARTESIAN_POINT ( 'NONE',  ( 4.052424581287595196, 3.786734753434853662, 0.5771415817955924954 ) ) ;
#12805=DIRECTION ( 'NONE',  ( 1.000000000000000000, 0.000000000000000000, 0.000000000000000000 ) ) ;
#12808=EDGE_LOOP ( 'NONE', ( #18534, #2494, #5855, #7886, #732 ) ) ;
#12822=CIRCLE ( 'NONE', #4371, 3.500000000000000000 ) ;
#12840=CARTESIAN_POINT ( 'NONE',  ( 4.114405500665256454, 4.051151509359430136, -5.737475420082528345E-17 ) ) ;
#12842=FACE_OUTER_BOUND ( 'NONE', #8399, .T. ) ;
#12843=CARTESIAN_POINT ( 'NONE',  ( 0.03027795055833727364, 0.6888063905328611902, 3.500000000000000888 ) ) ;
#12853=ADVANCED_FACE ( 'NONE', ( #14314 ), #255, .T. ) ;
#12868=CARTESIAN_POINT ( 'NONE',  ( 0.000000000000000000, -3.031088913245531202, 1.750000000000006439 ) ) ;
#12891=B_SPLINE_CURVE_WITH_KNOTS ( 'NONE', 3,
 ( #1849, #13796, #18332, #7023 ),
 .UNSPECIFIED., .F., .F.,
 ( 4, 4 ),
 ( 0.002080789711329271950, 0.004173039763574510827 ),
 .UNSPECIFIED. ) ;
#12929=CARTESIAN_POINT ( 'NONE',  ( 3.972709601346592123, 3.429395227388311262, 1.191688283765307332 ) ) ;
#12970=EDGE_LOOP ( 'NONE', ( #18682, #11113, #15538 ) ) ;
#13022=ORIENTED_EDGE ( 'NONE', *, *, #5099, .T. ) ;
#13030=EDGE_CURVE ( 'NONE', #16278, #606, #2456, .T. ) ;
#13045=B_SPLINE_CURVE_WITH_KNOTS ( 'NONE', 3,
 ( #10021, #13627, #14805, #5892, #18159 ),
 .UNSPECIFIED., .F., .F.,
 ( 4, 1, 4 ),
 ( 0.000000000000000000, 0.002020725942163692675, 0.004041451884327385349 ),
 .UNSPECIFIED. ) ;
#13157=DIRECTION ( 'NONE',  ( -1.000000000000000000, 0.000000000000000000, -0.000000000000000000 ) ) ;
#13167=EDGE_LOOP ( 'NONE', ( #11545, #2757, #3584 ) ) ;
#13180=EDGE_LOOP ( 'NONE', ( #16356, #15179, #5119, #8885, #13022, #8345, #18505 ) ) ;
#13191=CARTESIAN_POINT ( 'NONE',  ( 4.175813232069148562, -2.061359961916374051, -3.570380186727397653 ) ) ;
#13239=CARTESIAN_POINT ( 'NONE',  ( 4.175326769692856210, -2.060699556488920337, -3.569236330973475813 ) ) ;
#13280=CARTESIAN_POINT ( 'NONE',  ( 45.15499999999999403, 0.000000000000000000, 0.000000000000000000 ) ) ;
#13285=DIRECTION ( 'NONE',  ( -0.000000000000000000, 0.000000000000000000, -1.000000000000000000 ) ) ;
#13309=CIRCLE ( 'NONE', #1422, 3.500000000000000000 ) ;
#13329=CARTESIAN_POINT ( 'NONE',  ( 4.142654963991852846, -2.035398498734352746, -3.525413613457307971 ) ) ;
#13348=CARTESIAN_POINT ( 'NONE',  ( 3.973110223767137850, 2.263269463293572928E-11, 3.565797985667434222 ) ) ;
#13394=TOROIDAL_SURFACE ( 'NONE', #2776, 5.200000000000001066, 0.4999999999999978351 ) ;
#13404=CARTESIAN_POINT ( 'NONE',  ( 5.599999999999999645, -2.020725942163694722, -3.499999999999999556 ) ) ;
#13408=CIRCLE ( 'NONE', #3095, 3.500000000000000000 ) ;
#13411=ORIENTED_EDGE ( 'NONE', *, *, #18157, .F. ) ;
#13415=EDGE_CURVE ( 'NONE', #11423, #14693, #18576, .T. ) ;
#13437=CARTESIAN_POINT ( 'NONE',  ( 3.948103430091020272, 2.682758828852976229, -2.353325403973173024 ) ) ;
#13443=EDGE_LOOP ( 'NONE', ( #4976, #14588, #2017, #8528, #2666 ) ) ;
#13449=DIRECTION ( 'NONE',  ( 0.000000000000000000, 0.000000000000000000, -1.000000000000000000 ) ) ;
#13454=CARTESIAN_POINT ( 'NONE',  ( 4.052424581287701777, -3.786734753435149425, -0.5771415817957858962 ) ) ;
#13491=VERTEX_POINT ( 'NONE', #10371 ) ;
#13493=FACE_OUTER_BOUND ( 'NONE', #6824, .T. ) ;
#13548=DIRECTION ( 'NONE',  ( 0.000000000000000000, 0.000000000000000000, -1.000000000000000000 ) ) ;
#13553=CARTESIAN_POINT ( 'NONE',  ( 4.180231891692620216, -2.049421325483211653, -3.591231015387276848 ) ) ;
#13576=EDGE_CURVE ( 'NONE', #16928, #2243, #1227, .T. ) ;
#13581=CARTESIAN_POINT ( 'NONE',  ( 3.973514160553462737, -3.435084588004193140, 1.181876024140318782 ) ) ;
#13615=UNCERTAINTY_MEASURE_WITH_UNIT (LENGTH_MEASURE( 1.000000000000000082E-05 ), #10846, 'distance_accuracy_value', 'NONE');
#13624=AXIS2_PLACEMENT_3D ( 'NONE', #11191, #9723, #3661 ) ;
#13627=CARTESIAN_POINT ( 'NONE',  ( 3.951447005078453589, -3.704664227300103807, 0.5833333333333329263 ) ) ;
#13628=ORIENTED_EDGE ( 'NONE', *, *, #5099, .F. ) ;
#13648=AXIS2_PLACEMENT_3D ( 'NONE', #6731, #3418, #12715 ) ;
#13699=CONICAL_SURFACE ( 'NONE', #16837, 3.500000000000000000, 1.047197551196600296 ) ;
#13711=CARTESIAN_POINT ( 'NONE',  ( 5.100000000000002309, 0.000000000000000000, 0.000000000000000000 ) ) ;
#13715=AXIS2_PLACEMENT_3D ( 'NONE', #5701, #11273, #9897 ) ;
#13730=DIRECTION ( 'NONE',  ( 0.000000000000000000, 0.000000000000000000, -1.000000000000000000 ) ) ;
#13750=CARTESIAN_POINT ( 'NONE',  ( 4.071447262713887127, -2.020725942163686284, 3.500000000000000444 ) ) ;
#13782=( NAMED_UNIT ( * ) PLANE_ANGLE_UNIT ( ) SI_UNIT ( $, .RADIAN. ) );
#13790=ORIENTED_EDGE ( 'NONE', *, *, #294, .F. ) ;
#13793=SURFACE_SIDE_STYLE ('',( #6252 ) ) ;
#13796=CARTESIAN_POINT ( 'NONE',  ( 3.973110223765528026, -0.6902454861566464928, 3.565797985667392034 ) ) ;
#13825=CARTESIAN_POINT ( 'NONE',  ( 3.972709601346591235, 2.746729940827189242, -2.374099244652734697 ) ) ;
#13873=CARTESIAN_POINT ( 'NONE',  ( 4.082498951862918446, 2.020725942163685396, -3.500000000000001332 ) ) ;
#13895=AXIS2_PLACEMENT_3D ( 'NONE', #5316, #13157, #7177 ) ;
#13909=AXIS2_PLACEMENT_3D ( 'NONE', #2950, #17661, #7258 ) ;
#13921=CARTESIAN_POINT ( 'NONE',  ( 4.071447262713887127, -2.020725942163686284, 3.500000000000000444 ) ) ;
#13953=ORIENTED_EDGE ( 'NONE', *, *, #6378, .T. ) ;
#13958=ORIENTED_EDGE ( 'NONE', *, *, #18157, .T. ) ;
#13963=CARTESIAN_POINT ( 'NONE',  ( 4.132952817037861770, -4.063368025374527015, 6.968404583626299416E-17 ) ) ;
#13970=ADVANCED_FACE ( 'NONE', ( #2335 ), #6230, .T. ) ;
#13982=AXIS2_PLACEMENT_3D ( 'NONE', #1958, #3519, #9483 ) ;
#13999=LINE ( 'NONE', #12346, #14379 ) ;
#14005=VECTOR ( 'NONE', #814, 1000.000000000000000 ) ;
#14008=CARTESIAN_POINT ( 'NONE',  ( 4.071447262713887127, 2.020725942163688504, 3.500000000000000000 ) ) ;
#14016=CARTESIAN_POINT ( 'NONE',  ( 5.100000000000002309, 0.000000000000000000, 0.000000000000000000 ) ) ;
#14028=CARTESIAN_POINT ( 'NONE',  ( 5.599999999999998757, 0.000000000000000000, 5.200000000000001066 ) ) ;
#14030=EDGE_CURVE ( 'NONE', #14839, #3297, #3317, .T. ) ;
#14054=VERTEX_POINT ( 'NONE', #7215 ) ;
#14081=ORIENTED_EDGE ( 'NONE', *, *, #344, .T. ) ;
#14090=DIRECTION ( 'NONE',  ( 0.000000000000000000, 0.000000000000000000, 1.000000000000000000 ) ) ;
#14158=CARTESIAN_POINT ( 'NONE',  ( 3.972066048304770725, 3.435565134476467275, 1.180968096049824556 ) ) ;
#14216=VERTEX_POINT ( 'NONE', #1723 ) ;
#14253=CARTESIAN_POINT ( 'NONE',  ( 3.974167765203684866, 0.7238254970431302615, -3.565825589389262085 ) ) ;
#14256=CARTESIAN_POINT ( 'NONE',  ( 4.175326769692854434, 2.060699556488891027, -3.569236330973487803 ) ) ;
#14298=ORIENTED_EDGE ( 'NONE', *, *, #16708, .T. ) ;
#14299=CIRCLE ( 'NONE', #13982, 5.371010071662833063 ) ;
#14304=DIRECTION ( 'NONE',  ( 0.000000000000000000, 0.000000000000000000, 1.000000000000000000 ) ) ;
#14305=CARTESIAN_POINT ( 'NONE',  ( 4.093692494532771953, 4.043567292011543302, -5.737475420082528345E-17 ) ) ;
#14314=FACE_OUTER_BOUND ( 'NONE', #4250, .T. ) ;
#14326=CARTESIAN_POINT ( 'NONE',  ( 4.052424581287827010, -2.393186648133491357, 2.990837702970496892 ) ) ;
#14337=CARTESIAN_POINT ( 'NONE',  ( 4.050480423730738799, 1.376911654797411400, -3.567926555162023394 ) ) ;
#14379=VECTOR ( 'NONE', #687, 1000.000000000000000 ) ;
#14390=CARTESIAN_POINT ( 'NONE',  ( 4.050823680195223098, 2.400527758044901372, 2.978030508226146900 ) ) ;
#14406=CARTESIAN_POINT ( 'NONE',  ( 0.2182387239031248760, 1.693823289467350168, 3.500000000000000000 ) ) ;
#14422=ADVANCED_FACE ( 'NONE', ( #17211 ), #18495, .F. ) ;
#14432=CARTESIAN_POINT ( 'NONE',  ( 3.958484000407985981, -2.327740518749076948, 2.968235154689861321 ) ) ;
#14446=ORIENTED_EDGE ( 'NONE', *, *, #186, .F. ) ;
#14489=CARTESIAN_POINT ( 'NONE',  ( 0.000000000000000000, 0.000000000000000000, 2.500000000000000444 ) ) ;
#14502=DIRECTION ( 'NONE',  ( 0.000000000000000000, 0.5000000000000018874, 0.8660254037844375974 ) ) ;
#14528=AXIS2_PLACEMENT_3D ( 'NONE', #9028, #1692, #13449 ) ;
#14539=EDGE_CURVE ( 'NONE', #19337, #13491, #5044, .T. ) ;
#14588=ORIENTED_EDGE ( 'NONE', *, *, #5704, .T. ) ;
#14606=PRODUCT_CONTEXT ( 'NONE', #10873, 'mechanical' ) ;
#14640=CARTESIAN_POINT ( 'NONE',  ( 0.000000000000000000, 3.031088913245533867, 1.750000000000002887 ) ) ;
#14660=APPLICATION_CONTEXT ( 'automotive_design' ) ;
#14686=CARTESIAN_POINT ( 'NONE',  ( 0.000000000000000000, 0.000000000000000000, 0.000000000000000000 ) ) ;
#14693=VERTEX_POINT ( 'NONE', #6279 ) ;
#14703=CARTESIAN_POINT ( 'NONE',  ( 4.165266963751721008, -2.049631966911996006, -3.550066703508900190 ) ) ;
#14712=ADVANCED_FACE ( 'NONE', ( #15295 ), #12503, .T. ) ;
#14743=CARTESIAN_POINT ( 'NONE',  ( 0.02993401039713550899, 2.688325911136453250, -2.343682934607766111 ) ) ;
#14759=DIRECTION ( 'NONE',  ( 0.000000000000000000, -1.073081856240829552E-16, -1.000000000000000000 ) ) ;
#14780=ORIENTED_EDGE ( 'NONE', *, *, #4368, .T. ) ;
#14805=CARTESIAN_POINT ( 'NONE',  ( 3.806834918298644954, -3.031088913245536975, 1.750000000000000666 ) ) ;
#14806=EDGE_CURVE ( 'NONE', #16928, #4766, #13999, .T. ) ;
#14824=CARTESIAN_POINT ( 'NONE',  ( 4.030867648404857562, -3.732851566702167556, -0.5345114293585713217 ) ) ;
#14834=EDGE_LOOP ( 'NONE', ( #9806, #15339, #6900, #1843, #10687 ) ) ;
#14835=VECTOR ( 'NONE', #15522, 1000.000000000000000 ) ;
#14839=VERTEX_POINT ( 'NONE', #3922 ) ;
#14848=DIRECTION ( 'NONE',  ( 0.000000000000000000, 0.000000000000000000, 1.000000000000000000 ) ) ;
#14853=DIRECTION ( 'NONE',  ( -0.000000000000000000, 0.000000000000000000, -1.000000000000000000 ) ) ;
#14866=ORIENTED_EDGE ( 'NONE', *, *, #13030, .T. ) ;
#14874=CIRCLE ( 'NONE', #2991, 2.500000000000000444 ) ;
#14917=EDGE_CURVE ( 'NONE', #17135, #3297, #13408, .T. ) ;
#14925=CARTESIAN_POINT ( 'NONE',  ( 4.180345304246199767, -4.135116856707399258, 0.02129519942689610257 ) ) ;
#14972=CARTESIAN_POINT ( 'NONE',  ( 0.000000000000000000, 0.000000000000000000, 0.000000000000000000 ) ) ;
#14992=CARTESIAN_POINT ( 'NONE',  ( 4.086376042167606748, -1.979461949354202499, 3.571471332069183990 ) ) ;
#15003=DIRECTION ( 'NONE',  ( 0.000000000000000000, 0.000000000000000000, -1.000000000000000000 ) ) ;
#15023=CARTESIAN_POINT ( 'NONE',  ( 4.055492966679490330, -2.385006769472456156, -3.005124364834284023 ) ) ;
#15034=VERTEX_POINT ( 'NONE', #7628 ) ;
#15075=CARTESIAN_POINT ( 'NONE',  ( 4.175813232069150338, -4.122719923832746325, 2.362127131240695889E-16 ) ) ;
#15106=CARTESIAN_POINT ( 'NONE',  ( 4.055492966679587141, 3.795017426214561063, -0.5629142681441071661 ) ) ;
#15131=EDGE_LOOP ( 'NONE', ( #15726, #19316, #2985, #3120, #1637 ) ) ;
#15179=ORIENTED_EDGE ( 'NONE', *, *, #15270, .T. ) ;
#15221=CARTESIAN_POINT ( 'NONE',  ( 0.1381419387168661417, -1.355287006802423644, -3.499999999999999556 ) ) ;
#15226=CARTESIAN_POINT ( 'NONE',  ( 5.599999999999998757, 6.472876824008161592E-16, -5.200000000000001066 ) ) ;
#15270=EDGE_CURVE ( 'NONE', #1555, #19038, #12891, .T. ) ;
#15295=FACE_OUTER_BOUND ( 'NONE', #12970, .T. ) ;
#15304=CARTESIAN_POINT ( 'NONE',  ( 3.951447005078451813, 3.704664227300101143, 0.5833333333333334814 ) ) ;
#15327=CARTESIAN_POINT ( 'NONE',  ( 4.086262629614032527, -4.082406995609991540, -0.07093633357110748494 ) ) ;
#15339=ORIENTED_EDGE ( 'NONE', *, *, #15270, .F. ) ;
#15354=CARTESIAN_POINT ( 'NONE',  ( 4.142654963991859951, 2.035398498734348305, -3.525413613457315076 ) ) ;
#15356=AXIS2_PLACEMENT_3D ( 'NONE', #14972, #10261, #9089 ) ;
#15393=EDGE_CURVE ( 'NONE', #14693, #1555, #11003, .T. ) ;
#15400=CARTESIAN_POINT ( 'NONE',  ( 4.071447262713888016, 4.041451884327382338, 0.000000000000000000 ) ) ;
#15401=DIRECTION ( 'NONE',  ( -0.7071067811865533459, 0.000000000000000000, 0.7071067811865416886 ) ) ;
#15413=CARTESIAN_POINT ( 'NONE',  ( 0.02944718078674397194, -0.6813962075909725247, -3.500000000000000000 ) ) ;
#15425=( BOUNDED_SURFACE ( )  B_SPLINE_SURFACE ( 3, 2, ( 
 ( #11400, #8266, #9929 ),
 ( #5232, #17214, #3965 ),
 ( #15732, #6800, #11310 ),
 ( #15830, #631, #18789 ),
 ( #5337, #5520, #8365 ),
 ( #8073, #17312, #4066 ) ),
 .UNSPECIFIED., .F., .F., .F. ) 
 B_SPLINE_SURFACE_WITH_KNOTS ( ( 4, 2, 4 ),
 ( 3, 3 ),
 ( 0.01651732063679904258, 0.01857756227444016389, 0.02063780391208128520 ),
 ( 0.000000000000000000, 1.000000000000000000 ),
 .UNSPECIFIED. ) 
 GEOMETRIC_REPRESENTATION_ITEM ( )  RATIONAL_B_SPLINE_SURFACE ( (
 ( 1.000000000000000000, 0.8047781231227483234, 1.000000000000000000),
 ( 1.000000000000000000, 0.8123782108664983070, 1.000000000000000000),
 ( 1.000000000000000000, 0.8190665102133478648, 1.000000000000000000),
 ( 1.000000000000000000, 0.8192358432844011329, 1.000000000000000000),
 ( 1.000000000000000000, 0.8126132624435309371, 1.000000000000000000),
 ( 1.000000000000000000, 0.8047712436238877443, 1.000000000000000000) ) ) 
 REPRESENTATION_ITEM ( '' )  SURFACE ( )  );
#15446=FACE_OUTER_BOUND ( 'NONE', #6527, .T. ) ;
#15449=CARTESIAN_POINT ( 'NONE',  ( 4.086376042167606748, 4.082715877136863902, -0.07147133206917800907 ) ) ;
#15488=ADVANCED_FACE ( 'NONE', ( #13493 ), #16442, .F. ) ;
#15512=CARTESIAN_POINT ( 'NONE',  ( 4.158413352280813768, -2.044871626972823542, 3.541821552872969736 ) ) ;
#15522=DIRECTION ( 'NONE',  ( -1.000000000000000000, -0.000000000000000000, -0.000000000000000000 ) ) ;
#15533=CARTESIAN_POINT ( 'NONE',  ( 4.050536630291690088, -2.401306687817039265, 2.976670123173768445 ) ) ;
#15534=B_SPLINE_CURVE_WITH_KNOTS ( 'NONE', 3,
 ( #4221, #8630, #13239, #10099, #1192, #14703, #2959, #4322, #13329, #19250, #17762, #1093, #7358, #17476, #19349, #10290 ),
 .UNSPECIFIED., .F., .F.,
 ( 4, 3, 3, 3, 3, 4 ),
 ( -2.111273352581287704E-06, 0.000000000000000000, 3.519286887794526448E-05, 7.191842652068348909E-05, 0.0001049868727093649664, 0.0001382836236822123786 ),
 .UNSPECIFIED. ) ;
#15538=ORIENTED_EDGE ( 'NONE', *, *, #6433, .T. ) ;
#15545=CARTESIAN_POINT ( 'NONE',  ( 4.165266963751724560, -4.099263933823990236, 4.401844587977598791E-16 ) ) ;
#15554=CARTESIAN_POINT ( 'NONE',  ( 0.000000000000000000, 3.031088913245533867, 1.750000000000002887 ) ) ;
#15600=DIRECTION ( 'NONE',  ( 0.000000000000000000, 0.000000000000000000, 1.000000000000000000 ) ) ;
#15627=ORIENTED_EDGE ( 'NONE', *, *, #18878, .T. ) ;
#15629=ORIENTED_EDGE ( 'NONE', *, *, #7288, .F. ) ;
#15675=EDGE_CURVE ( 'NONE', #19038, #18672, #8667, .T. ) ;
#15679=AXIS2_PLACEMENT_3D ( 'NONE', #13711, #9108, #18048 ) ;
#15726=ORIENTED_EDGE ( 'NONE', *, *, #14806, .F. ) ;
#15732=CARTESIAN_POINT ( 'NONE',  ( 3.880214671983734043, -0.7309020039772819999, 3.500000000000000444 ) ) ;
#15738=ORIENTED_EDGE ( 'NONE', *, *, #3836, .F. ) ;
#15768=ADVANCED_FACE ( 'NONE', ( #9171 ), #15425, .F. ) ;
#15790=CARTESIAN_POINT ( 'NONE',  ( 5.599999999999998757, 0.000000000000000000, 0.000000000000000000 ) ) ;
#15794=CARTESIAN_POINT ( 'NONE',  ( 4.151274195509679465, 2.039912954708742898, 3.533232880573493606 ) ) ;
#15796=CARTESIAN_POINT ( 'NONE',  ( 45.15499999999999403, 0.000000000000000000, 2.500000000000000444 ) ) ;
#15810=CARTESIAN_POINT ( 'NONE',  ( 4.175326769692855322, -2.060699556488924333, 3.569236330973470928 ) ) ;
#15813=CARTESIAN_POINT ( 'NONE',  ( 3.948103430090711630, -2.682758828852738642, 2.353325403972896357 ) ) ;
#15830=CARTESIAN_POINT ( 'NONE',  ( 3.878089031707363521, 0.7015470581914173831, 3.500000000000000444 ) ) ;
#15850=CARTESIAN_POINT ( 'NONE',  ( 0.000000000000000000, 0.000000000000000000, 0.000000000000000000 ) ) ;
#15888=CARTESIAN_POINT ( 'NONE',  ( 4.175813232069148562, 4.122719923832741884, -2.765695189283172261E-17 ) ) ;
#15894=CARTESIAN_POINT ( 'NONE',  ( 3.951447005078454477, -3.704664227300105583, -0.5833333333333333703 ) ) ;
#15919=EDGE_CURVE ( 'NONE', #17135, #5826, #12822, .T. ) ;
#15958=EDGE_LOOP ( 'NONE', ( #15981, #17841, #13411, #17362 ) ) ;
#15977=DIRECTION ( 'NONE',  ( -1.000000000000000000, -0.000000000000000000, -0.000000000000000000 ) ) ;
#15981=ORIENTED_EDGE ( 'NONE', *, *, #8447, .T. ) ;
#15984=CARTESIAN_POINT ( 'NONE',  ( 4.082498951862917558, 4.041451884327382338, 3.558567857214853949E-17 ) ) ;
#15989=CARTESIAN_POINT ( 'NONE',  ( 4.104070371397480876, 2.023683613428366002, 3.505122836902507810 ) ) ;
#15992=CARTESIAN_POINT ( 'NONE',  ( 0.1388410611046087539, 3.710337782248032568, 0.5735064479039790886 ) ) ;
#15993=CONICAL_SURFACE ( 'NONE', #2849, 3.500000000000000000, 1.047197551196600296 ) ;
#16016=FACE_OUTER_BOUND ( 'NONE', #11833, .T. ) ;
#16054=ORIENTED_EDGE ( 'NONE', *, *, #8002, .T. ) ;
#16086=CARTESIAN_POINT ( 'NONE',  ( 4.175075985190098038, 4.120741555260245548, 3.964526709274768569E-16 ) ) ;
#16124=DIRECTION ( 'NONE',  ( -1.000000000000000000, -0.000000000000000000, -0.000000000000000000 ) ) ;
#16139=EDGE_CURVE ( 'NONE', #6054, #14216, #10391, .T. ) ;
#16141=DIRECTION ( 'NONE',  ( 0.000000000000000000, -0.5000000000000004441, 0.8660254037844383745 ) ) ;
#16165=CARTESIAN_POINT ( 'NONE',  ( 0.000000000000000000, 0.000000000000000000, 0.000000000000000000 ) ) ;
#16191=DIRECTION ( 'NONE',  ( 1.000000000000000000, 0.000000000000000000, 0.000000000000000000 ) ) ;
#16261=CARTESIAN_POINT ( 'NONE',  ( 3.951447005078451813, -1.347150628109131443, -3.500000000000000444 ) ) ;
#16278=VERTEX_POINT ( 'NONE', #17291 ) ;
#16322=CARTESIAN_POINT ( 'NONE',  ( 0.000000000000000000, 0.000000000000000000, 0.000000000000000000 ) ) ;
#16346=CARTESIAN_POINT ( 'NONE',  ( 5.599999999999999645, 2.020725942163688504, 3.500000000000000000 ) ) ;
#16356=ORIENTED_EDGE ( 'NONE', *, *, #9976, .F. ) ;
#16361=CYLINDRICAL_SURFACE ( 'NONE', #12134, 2.500000000000000444 ) ;
#16402=CARTESIAN_POINT ( 'NONE',  ( 0.1217565302851118803, -3.710888496608922171, 0.5725525826504672677 ) ) ;
#16409=FACE_OUTER_BOUND ( 'NONE', #15958, .T. ) ;
#16442=PLANE ( 'NONE',  #16570 ) ;
#16500=FACE_OUTER_BOUND ( 'NONE', #18255, .T. ) ;
#16506=CARTESIAN_POINT ( 'NONE',  ( 3.961551342853212532, -2.319461885623237851, -2.982574167881048677 ) ) ;
#16556=DIRECTION ( 'NONE',  ( -1.000000000000000000, -0.000000000000000000, -0.000000000000000000 ) ) ;
#16570=AXIS2_PLACEMENT_3D ( 'NONE', #16346, #14759, #1642 ) ;
#16604=CARTESIAN_POINT ( 'NONE',  ( 4.158921614371310582, -4.076055977742308656, 0.05993604794450350243 ) ) ;
#16669=ORIENTED_EDGE ( 'NONE', *, *, #16139, .F. ) ;
#16706=CARTESIAN_POINT ( 'NONE',  ( 0.3126073911695746443, -2.020725942163797750, -3.499999999999999556 ) ) ;
#16708=EDGE_CURVE ( 'NONE', #11235, #11423, #4081, .T. ) ;
#16730=ADVANCED_FACE ( 'NONE', ( #7752 ), #6270, .T. ) ;
#16734=DIRECTION ( 'NONE',  ( 1.000000000000000000, 0.000000000000000000, 0.000000000000000000 ) ) ;
#16753=CONICAL_SURFACE ( 'NONE', #452, 5.371010071662833063, 1.221730476396037490 ) ;
#16765=AXIS2_PLACEMENT_3D ( 'NONE', #497, #2070, #6373 ) ;
#16817=ORIENTED_EDGE ( 'NONE', *, *, #4125, .T. ) ;
#16835=CARTESIAN_POINT ( 'NONE',  ( 4.158921444904715159, -2.089933220600048713, -3.500000000000000000 ) ) ;
#16837=AXIS2_PLACEMENT_3D ( 'NONE', #14686, #7045, #10081 ) ;
#16842=ADVANCED_FACE ( 'NONE', ( #16984 ), #6464, .F. ) ;
#16844=CARTESIAN_POINT ( 'NONE',  ( 4.630153689607048761, 6.577590292450083844E-16, 5.371010071662833063 ) ) ;
#16851=SHAPE_REPRESENTATION_RELATIONSHIP ( 'NONE' , 'NONE' ,  #1297, #6165 ) ;
#16913=CARTESIAN_POINT ( 'NONE',  ( 3.973110223767137850, -2.261493176400255405E-11, -3.565797985667433334 ) ) ;
#16928=VERTEX_POINT ( 'NONE', #7608 ) ;
#16956=CARTESIAN_POINT ( 'NONE',  ( 0.000000000000000000, -3.031088913245534755, -1.750000000000001332 ) ) ;
#16957=EDGE_CURVE ( 'NONE', #468, #3703, #7418, .T. ) ;
#16984=FACE_OUTER_BOUND ( 'NONE', #12808, .T. ) ;
#17014=CARTESIAN_POINT ( 'NONE',  ( 4.050880675075948290, -1.379097446046192665, -3.567934390854430315 ) ) ;
#17024=CARTESIAN_POINT ( 'NONE',  ( 4.050823680195226650, -3.779313952391382792, 0.5899027668435167238 ) ) ;
#17032=CARTESIAN_POINT ( 'NONE',  ( 4.052416734886645777, -1.393505408945131308, -3.567979131523694836 ) ) ;
#17034=CARTESIAN_POINT ( 'NONE',  ( 4.093692494532774617, 2.021783646005766322, -3.501831996793843160 ) ) ;
#17055=B_SPLINE_CURVE_WITH_KNOTS ( 'NONE', 3,
 ( #12868, #1573, #4311, #5987, #7446, #1372 ),
 .UNSPECIFIED., .F., .F.,
 ( 4, 2, 4 ),
 ( 0.002044882221487539717, 0.003063384235218500652, 0.004081886248949461587 ),
 .UNSPECIFIED. ) ;
#17111=ORIENTED_EDGE ( 'NONE', *, *, #6051, .F. ) ;
#17135=VERTEX_POINT ( 'NONE', #8325 ) ;
#17139=CIRCLE ( 'NONE', #8669, 5.371010071662833063 ) ;
#17144=CARTESIAN_POINT ( 'NONE',  ( 0.2174200650117580902, -3.876582599186216616, -0.2855619784720681564 ) ) ;
#17161=( GEOMETRIC_REPRESENTATION_CONTEXT ( 3 ) GLOBAL_UNCERTAINTY_ASSIGNED_CONTEXT ( ( #9500 ) ) GLOBAL_UNIT_ASSIGNED_CONTEXT ( ( #7803, #13782, #372 ) ) REPRESENTATION_CONTEXT ( 'NONE', 'WORKASPACE' ) );
#17200=CARTESIAN_POINT ( 'NONE',  ( 5.100000000000002309, 0.000000000000000000, 5.200000000000001066 ) ) ;
#17209=ORIENTED_EDGE ( 'NONE', *, *, #15675, .F. ) ;
#17211=FACE_OUTER_BOUND ( 'NONE', #8028, .T. ) ;
#17214=CARTESIAN_POINT ( 'NONE',  ( 4.033906725095553369, -1.419670120619691334, 3.500000000000000444 ) ) ;
#17224=CARTESIAN_POINT ( 'NONE',  ( 3.961551342853837809, 2.319461885623310682, 2.982574167880912341 ) ) ;
#17255=EDGE_CURVE ( 'NONE', #7505, #7529, #6907, .T. ) ;
#17267=CARTESIAN_POINT ( 'NONE',  ( 0.000000000000000000, 0.000000000000000000, 0.000000000000000000 ) ) ;
#17291=CARTESIAN_POINT ( 'NONE',  ( 5.599999999999999645, 0.000000000000000000, 2.500000000000000444 ) ) ;
#17293=CARTESIAN_POINT ( 'NONE',  ( 4.104070371397484429, -2.023683613428364669, 3.505122836902509587 ) ) ;
#17312=CARTESIAN_POINT ( 'NONE',  ( 4.158921784487744411, 2.089935040870091409, 3.500000000000000444 ) ) ;
#17330=CARTESIAN_POINT ( 'NONE',  ( 45.15499999999999403, 3.061616997868383634E-16, -2.500000000000000444 ) ) ;
#17362=ORIENTED_EDGE ( 'NONE', *, *, #6804, .F. ) ;
#17415=CARTESIAN_POINT ( 'NONE',  ( 0.3126073911696399255, 2.020725942163686284, -3.499999999999999556 ) ) ;
#17465=CARTESIAN_POINT ( 'NONE',  ( 0.000000000000000000, 0.000000000000000000, -3.499999999999999556 ) ) ;
#17476=CARTESIAN_POINT ( 'NONE',  ( 4.093692494532771953, -2.021783646005774759, -3.501831996793842716 ) ) ;
#17518=DIRECTION ( 'NONE',  ( -0.000000000000000000, 0.8660254037844383745, 0.5000000000000004441 ) ) ;
#17522=CARTESIAN_POINT ( 'NONE',  ( 45.60000000000000142, 0.000000000000000000, 0.000000000000000000 ) ) ;
#17527=CARTESIAN_POINT ( 'NONE',  ( 0.1217565302851095904, 2.351289329882149559, 2.927447417349536618 ) ) ;
#17555=ADVANCED_FACE ( 'NONE', ( #3144 ), #4726, .T. ) ;
#17559=ORIENTED_EDGE ( 'NONE', *, *, #7288, .T. ) ;
#17562=EDGE_CURVE ( 'NONE', #6796, #7366, #3329, .T. ) ;
#17572=CARTESIAN_POINT ( 'NONE',  ( 4.175572532730931208, 2.061029303918050726, 3.569807470274392713 ) ) ;
#17626=CARTESIAN_POINT ( 'NONE',  ( 45.60000000000000142, 2.789133085058097101E-16, -2.055000000000000160 ) ) ;
#17661=DIRECTION ( 'NONE',  ( 0.000000000000000000, -0.8660254037844380415, 0.5000000000000012212 ) ) ;
#17709=CARTESIAN_POINT ( 'NONE',  ( 4.175813232069148562, -2.061359961916374051, -3.570380186727397653 ) ) ;
#17762=CARTESIAN_POINT ( 'NONE',  ( 4.124214193018069352, -2.028338413290947440, -3.513185186763551737 ) ) ;
#17782=EDGE_CURVE ( 'NONE', #19337, #19038, #9242, .T. ) ;
#17789=EDGE_LOOP ( 'NONE', ( #12490, #11735, #11621, #9074 ) ) ;
#17813=DIRECTION ( 'NONE',  ( 0.000000000000000000, 0.000000000000000000, 1.000000000000000000 ) ) ;
#17815=ORIENTED_EDGE ( 'NONE', *, *, #4368, .F. ) ;
#17831=FACE_OUTER_BOUND ( 'NONE', #17789, .T. ) ;
#17841=ORIENTED_EDGE ( 'NONE', *, *, #5704, .F. ) ;
#17869=B_SPLINE_CURVE_WITH_KNOTS ( 'NONE', 3,
 ( #15075, #3593, #2231, #11122, #9554, #15545, #10930, #18801, #8378, #13963, #3788, #8278, #18702, #4957, #2124, #8190 ),
 .UNSPECIFIED., .F., .F.,
 ( 4, 3, 3, 3, 3, 4 ),
 ( -2.111273352579798197E-06, 0.000000000000000000, 3.519286887794736512E-05, 7.191842652068568460E-05, 0.0001049868727093669315, 0.0001382836236822145742 ),
 .UNSPECIFIED. ) ;
#17875=AXIS2_PLACEMENT_3D ( 'NONE', #11068, #4997, #11629 ) ;
#17916=EDGE_LOOP ( 'NONE', ( #10551, #6540, #750, #14446 ) ) ;
#17937=DIRECTION ( 'NONE',  ( 1.000000000000000000, 0.000000000000000000, -0.000000000000000000 ) ) ;
#17938=EDGE_CURVE ( 'NONE', #3703, #5826, #8967, .T. ) ;
#17954=B_SPLINE_CURVE_WITH_KNOTS ( 'NONE', 3,
 ( #19048, #10096, #5696, #15992, #18951, #5491 ),
 .UNSPECIFIED., .F., .F.,
 ( 4, 2, 4 ),
 ( 0.002044882221487525839, 0.003063384235218491979, 0.004081886248949458118 ),
 .UNSPECIFIED. ) ;
#17982=DIRECTION ( 'NONE',  ( -1.000000000000000000, -0.000000000000000000, -0.000000000000000000 ) ) ;
#17984=CARTESIAN_POINT ( 'NONE',  ( 3.972066048304772501, -3.435565134476469495, -1.180968096049828775 ) ) ;
#17986=CARTESIAN_POINT ( 'NONE',  ( 4.175813232069146785, -2.061359961916366057, 3.570380186727398542 ) ) ;
#18034=CARTESIAN_POINT ( 'NONE',  ( 4.071447262713888016, 4.041451884327382338, 0.000000000000000000 ) ) ;
#18048=DIRECTION ( 'NONE',  ( 0.000000000000000000, 0.000000000000000000, 1.000000000000000000 ) ) ;
#18051=CARTESIAN_POINT ( 'NONE',  ( 5.599999999999998757, 0.000000000000000000, 0.000000000000000000 ) ) ;
#18059=CARTESIAN_POINT ( 'NONE',  ( 4.180345304246196214, 2.049116244671343345, -3.591763845239305919 ) ) ;
#18128=CARTESIAN_POINT ( 'NONE',  ( 4.175813232069148562, -2.061359961916374051, -3.570380186727397653 ) ) ;
#18157=EDGE_CURVE ( 'NONE', #762, #10511, #15534, .T. ) ;
#18159=CARTESIAN_POINT ( 'NONE',  ( 4.071447262713887127, -2.020725942163686284, 3.500000000000000444 ) ) ;
#18163=VECTOR ( 'NONE', #16124, 1000.000000000000000 ) ;
#18168=CARTESIAN_POINT ( 'NONE',  ( 3.973514160553462737, 3.435084588004190476, -1.181876024140317227 ) ) ;
#18174=DIRECTION ( 'NONE',  ( 0.000000000000000000, 0.000000000000000000, 1.000000000000000000 ) ) ;
#18234=EDGE_LOOP ( 'NONE', ( #6042, #19406, #18665, #5869, #19171, #15738 ) ) ;
#18253=CARTESIAN_POINT ( 'NONE',  ( 0.000000000000000000, 0.000000000000000000, -3.499999999999999556 ) ) ;
#18255=EDGE_LOOP ( 'NONE', ( #3318, #4309, #4503, #11845, #15627, #14298, #7442 ) ) ;
#18298=AXIS2_PLACEMENT_3D ( 'NONE', #17200, #11096, #5034 ) ;
#18332=CARTESIAN_POINT ( 'NONE',  ( 4.050480423730737911, -1.376911654797406070, 3.567926555162024282 ) ) ;
#18377=CARTESIAN_POINT ( 'NONE',  ( 0.2175679805410235534, -1.691499766303381058, -3.499999999999999556 ) ) ;
#18403=CARTESIAN_POINT ( 'NONE',  ( 4.175813232069146785, -2.061359961916366057, 3.570380186727398542 ) ) ;
#18411=CARTESIAN_POINT ( 'NONE',  ( 4.055487192203242941, 1.409979666030558354, -3.568038521265956664 ) ) ;
#18415=CARTESIAN_POINT ( 'NONE',  ( 4.175813232069146785, 2.061359961916365613, -3.570380186727397653 ) ) ;
#18430=CARTESIAN_POINT ( 'NONE',  ( 4.630153689607048761, 6.577590292450083844E-16, 5.371010071662833063 ) ) ;
#18458=COLOUR_RGB ( '',1.000000000000000000, 0.9490196078431372140, 0.9098039215686274384 ) ;
#18459=CARTESIAN_POINT ( 'NONE',  ( 5.599999999999999645, 0.000000000000000000, 0.000000000000000000 ) ) ;
#18495=PLANE ( 'NONE',  #11241 ) ;
#18505=ORIENTED_EDGE ( 'NONE', *, *, #7879, .T. ) ;
#18516=ADVANCED_FACE ( 'NONE', ( #3984, #18907 ), #11422, .T. ) ;
#18534=ORIENTED_EDGE ( 'NONE', *, *, #8854, .F. ) ;
#18562=DIRECTION ( 'NONE',  ( 0.000000000000000000, 0.000000000000000000, -1.000000000000000000 ) ) ;
#18576=B_SPLINE_CURVE_WITH_KNOTS ( 'NONE', 3,
 ( #8612, #4111, #12929, #8410, #14390, #18932 ),
 .UNSPECIFIED., .F., .F.,
 ( 4, 2, 4 ),
 ( 0.000000000000000000, 0.002086519881787259317, 0.004173039763574518633 ),
 .UNSPECIFIED. ) ;
#18596=CARTESIAN_POINT ( 'NONE',  ( 5.599999999999999645, 2.020725942163686284, -3.499999999999999556 ) ) ;
#18608=CARTESIAN_POINT ( 'NONE',  ( 3.948103430090398991, 3.379418997638670596, 1.146674596026254322 ) ) ;
#18654=CARTESIAN_POINT ( 'NONE',  ( 4.104070371397481765, 4.047367226856738220, -5.737475420082528345E-17 ) ) ;
#18665=ORIENTED_EDGE ( 'NONE', *, *, #9615, .F. ) ;
#18669=CARTESIAN_POINT ( 'NONE',  ( 4.114405500665260895, -2.025575754679711071, 3.508400121684938089 ) ) ;
#18672=VERTEX_POINT ( 'NONE', #12296 ) ;
#18682=ORIENTED_EDGE ( 'NONE', *, *, #3205, .T. ) ;
#18698=CARTESIAN_POINT ( 'NONE',  ( 3.880198502136737115, 0.7307680362927179152, -3.499999999999999556 ) ) ;
#18701=CARTESIAN_POINT ( 'NONE',  ( 4.170895651974849017, 2.054890354522707074, -3.559174498016318910 ) ) ;
#18702=CARTESIAN_POINT ( 'NONE',  ( 4.104070371397483541, -4.047367226856742661, 3.293285021600925981E-16 ) ) ;
#18712=DIRECTION ( 'NONE',  ( 1.000000000000000000, 0.000000000000000000, 0.000000000000000000 ) ) ;
#18725=CARTESIAN_POINT ( 'NONE',  ( 0.000000000000000000, 3.031088913245533423, -1.750000000000004885 ) ) ;
#18728=CARTESIAN_POINT ( 'NONE',  ( 0.3126073911696407026, -2.020725942163686728, 3.500000000000000444 ) ) ;
#18735=CARTESIAN_POINT ( 'NONE',  ( 4.071447262713887127, 2.020725942163688504, 3.500000000000000000 ) ) ;
#18745=CARTESIAN_POINT ( 'NONE',  ( 4.071447262713887127, 2.020725942163688504, 3.500000000000000000 ) ) ;
#18769=PLANE ( 'NONE',  #13895 ) ;
#18789=CARTESIAN_POINT ( 'NONE',  ( 3.972058292797711054, 0.6948821373584146421, 3.565770528409240026 ) ) ;
#18800=CARTESIAN_POINT ( 'NONE',  ( 4.158413352280813768, 2.044871626972823986, -3.541821552872968404 ) ) ;
#18801=CARTESIAN_POINT ( 'NONE',  ( 4.151274195509681242, -4.079825909417492902, 4.401844587977598791E-16 ) ) ;
#18818=EDGE_LOOP ( 'NONE', ( #11451, #15629, #7341, #17209 ) ) ;
#18833=CARTESIAN_POINT ( 'NONE',  ( 0.2175679805369682140, -1.691499766289324080, 3.500000000000000000 ) ) ;
#18848=CARTESIAN_POINT ( 'NONE',  ( 4.132952817037860882, 4.063368025374523462, 1.253603594387587993E-15 ) ) ;
#18851=PLANE ( 'NONE',  #1084 ) ;
#18852=CARTESIAN_POINT ( 'NONE',  ( 4.175075985190095373, 2.060370777630105898, 3.568666869285574972 ) ) ;
#18878=EDGE_CURVE ( 'NONE', #6796, #11235, #10598, .T. ) ;
#18907=FACE_OUTER_BOUND ( 'NONE', #3994, .T. ) ;
#18927=CARTESIAN_POINT ( 'NONE',  ( 0.1381419387119174058, -1.355287006778759018, 3.500000000000000888 ) ) ;
#18932=CARTESIAN_POINT ( 'NONE',  ( 4.175813232069147674, 2.061359961916367833, 3.570380186727398097 ) ) ;
#18947=CARTESIAN_POINT ( 'NONE',  ( 5.599999999999999645, -4.041451884327386779, 0.000000000000000000 ) ) ;
#18949=CARTESIAN_POINT ( 'NONE',  ( 4.093692494532771953, 2.021783646005768542, 3.501831996793843160 ) ) ;
#18951=CARTESIAN_POINT ( 'NONE',  ( 0.2174200650117547873, 3.876582599186211731, 0.2855619784720684895 ) ) ;
#18986=ORIENTED_EDGE ( 'NONE', *, *, #7733, .T. ) ;
#18990=CARTESIAN_POINT ( 'NONE',  ( 0.2174200650117528444, 2.185595227304856891, -3.214438021527932676 ) ) ;
#19038=VERTEX_POINT ( 'NONE', #17986 ) ;
#19041=CARTESIAN_POINT ( 'NONE',  ( 0.2182387239012630320, 1.693823289460900883, -3.499999999999999112 ) ) ;
#19044=DIRECTION ( 'NONE',  ( 0.000000000000000000, 0.8660254037844375974, -0.5000000000000018874 ) ) ;
#19048=CARTESIAN_POINT ( 'NONE',  ( 0.000000000000000000, 3.031088913245533867, 1.750000000000002887 ) ) ;
#19103=ORIENTED_EDGE ( 'NONE', *, *, #4125, .F. ) ;
#19151=CARTESIAN_POINT ( 'NONE',  ( 3.806834918298644954, -3.031088913245541416, -1.749999999999998890 ) ) ;
#19171=ORIENTED_EDGE ( 'NONE', *, *, #14917, .T. ) ;
#19201=CARTESIAN_POINT ( 'NONE',  ( 5.599999999999999645, -2.020725942163694722, -3.499999999999999556 ) ) ;
#19238=CARTESIAN_POINT ( 'NONE',  ( 3.880206590543186618, -3.396506438958517116, 1.117078279489015502 ) ) ;
#19250=CARTESIAN_POINT ( 'NONE',  ( 4.132952817037859106, -2.031684012687264396, -3.518979934899745032 ) ) ;
#19269=B_SPLINE_CURVE_WITH_KNOTS ( 'NONE', 3,
 ( #3065, #6284, #6095, #19 ),
 .UNSPECIFIED., .F., .F.,
 ( 4, 4 ),
 ( 2.380739282773774244E-07, 0.002044882221487524104 ),
 .UNSPECIFIED. ) ;
#19300=DIRECTION ( 'NONE',  ( -1.000000000000000000, -0.000000000000000000, -0.000000000000000000 ) ) ;
#19316=ORIENTED_EDGE ( 'NONE', *, *, #13576, .T. ) ;
#19337=VERTEX_POINT ( 'NONE', #13921 ) ;
#19349=CARTESIAN_POINT ( 'NONE',  ( 4.082498951862917558, -2.020725942163694722, -3.499999999999999556 ) ) ;
#19403=ORIENTED_EDGE ( 'NONE', *, *, #4858, .T. ) ;
#19406=ORIENTED_EDGE ( 'NONE', *, *, #4848, .F. ) ;
#19469=COLOUR_RGB('Black',0.12,0.14,0.17);
#19470=FILL_AREA_STYLE_COLOUR('',#19469);
#19471=FILL_AREA_STYLE('',(#19470));
#19472=SURFACE_STYLE_FILL_AREA(#19471);
#19473=SURFACE_SIDE_STYLE('',(#19472));
#19474=SURFACE_STYLE_USAGE(.BOTH.,#19473);
#19475=PRESENTATION_STYLE_ASSIGNMENT((#19474));
ENDSEC;
END-ISO-10303-21;
